ISO-10303-21;
HEADER;
FILE_DESCRIPTION (('STEP AP214'),
    '1' );
FILE_NAME ('torque nut 01_iso_ISO 7040-M4-N.step',
    '2026-10-08T07:58:12',
    ( '' ),
    ( '' ),
    'SwSTEP 2.0',
    'SolidWorks 2026',
    '' );
FILE_SCHEMA (( 'AUTOMOTIVE_DESIGN' ));
ENDSEC;

DATA;
#5=ORIENTED_EDGE ( 'NONE', *, *, #16046, .F. ) ;
#22=SURFACE_SIDE_STYLE ('',( #2407 ) ) ;
#47=EDGE_LOOP ( 'NONE', ( #1882, #26577, #33467, #1949, #7115, #1431 ) ) ;
#81=CARTESIAN_POINT ( 'NONE',  ( -0.2855619784720687115, 3.876582599186216616, -0.2174200650117638633 ) ) ;
#115=EDGE_CURVE ( 'NONE', #13221, #23693, #5798, .T. ) ;
#132=DIRECTION ( 'NONE',  ( 1.000000000000000000, 0.000000000000000000, 0.000000000000000000 ) ) ;
#201=CARTESIAN_POINT ( 'NONE',  ( 0.000000000000000000, 0.000000000000000000, 2.066666666667000385 ) ) ;
#220=AXIS2_PLACEMENT_3D ( 'NONE', #21698, #13527, #16251 ) ;
#235=EDGE_CURVE ( 'NONE', #32873, #16396, #27571, .T. ) ;
#243=CARTESIAN_POINT ( 'NONE',  ( 3.469446951953614189E-15, -4.041451884327432076, -2.899999999999999911 ) ) ;
#258=VERTEX_POINT ( 'NONE', #32202 ) ;
#285=ORIENTED_EDGE ( 'NONE', *, *, #11593, .T. ) ;
#371=ORIENTED_EDGE ( 'NONE', *, *, #28490, .F. ) ;
#382=CIRCLE ( 'NONE', #1466, 1.033333333332998372 ) ;
#397=CIRCLE ( 'NONE', #9630, 3.499999999999999556 ) ;
#404=ORIENTED_EDGE ( 'NONE', *, *, #3314, .F. ) ;
#418=PLANE ( 'NONE',  #220 ) ;
#446=ADVANCED_FACE ( 'NONE', ( #17719 ), #1879, .F. ) ;
#567=ORIENTED_EDGE ( 'NONE', *, *, #11593, .F. ) ;
#570=FACE_OUTER_BOUND ( 'NONE', #15244, .T. ) ;
#574=EDGE_CURVE ( 'NONE', #21522, #10366, #23665, .T. ) ;
#579=DIRECTION ( 'NONE',  ( 1.000000000000000000, 1.776356839400250465E-15, 0.000000000000000000 ) ) ;
#605=DIRECTION ( 'NONE',  ( -0.000000000000000000, -0.000000000000000000, 1.000000000000000000 ) ) ;
#617=FACE_OUTER_BOUND ( 'NONE', #6434, .T. ) ;
#697=VERTEX_POINT ( 'NONE', #18883 ) ;
#723=EDGE_CURVE ( 'NONE', #697, #15536, #20846, .T. ) ;
#728=CIRCLE ( 'NONE', #9429, 2.000000000000000888 ) ;
#733=CARTESIAN_POINT ( 'NONE',  ( 3.500000000000004441, -0.6807265984995718444, -0.02935130719647200889 ) ) ;
#781=DIRECTION ( 'NONE',  ( 0.000000000000000000, 0.000000000000000000, -1.000000000000000000 ) ) ;
#946=AXIS2_PLACEMENT_3D ( 'NONE', #5551, #781, #28896 ) ;
#964=CARTESIAN_POINT ( 'NONE',  ( -3.499999999999999556, -0.6807265984995715113, -0.02935130719646900088 ) ) ;
#1072=CARTESIAN_POINT ( 'NONE',  ( 3.499999999999993339, -2.020725942163723143, -0.3126073911696551910 ) ) ;
#1090=CARTESIAN_POINT ( 'NONE',  ( 0.000000000000000000, 0.000000000000000000, -2.899999999999999911 ) ) ;
#1172=FACE_OUTER_BOUND ( 'NONE', #23032, .T. ) ;
#1179=CARTESIAN_POINT ( 'NONE',  ( -3.214438021527937117, -2.185595227304884425, -2.682579934988229997 ) ) ;
#1265=AXIS2_PLACEMENT_3D ( 'NONE', #21852, #8910, #19303 ) ;
#1272=CARTESIAN_POINT ( 'NONE',  ( 1.750000000000016209, -3.031088913245524985, -2.899999999999999911 ) ) ;
#1301=CIRCLE ( 'NONE', #14892, 2.000000000000000888 ) ;
#1302=PRESENTATION_STYLE_ASSIGNMENT (( #24286 ) ) ;
#1330=CARTESIAN_POINT ( 'NONE',  ( -1.750000000000014211, 3.031088913245526317, -2.899999999999999911 ) ) ;
#1334=EDGE_CURVE ( 'NONE', #258, #1780, #13570, .T. ) ;
#1353=CARTESIAN_POINT ( 'NONE',  ( -1.750000000000016209, -3.031088913245524985, -2.899999999999999911 ) ) ;
#1376=CARTESIAN_POINT ( 'NONE',  ( 0.000000000000000000, 0.000000000000000000, 9.480888224575629408 ) ) ;
#1389=CARTESIAN_POINT ( 'NONE',  ( -3.499999999999996891, 4.286263797015732651E-16, 9.480888224575629408 ) ) ;
#1423=EDGE_CURVE ( 'NONE', #13631, #32991, #13115, .T. ) ;
#1428=CARTESIAN_POINT ( 'NONE',  ( 3.500000000000004885, 0.6879904500768362352, -2.869836757075876488 ) ) ;
#1431=ORIENTED_EDGE ( 'NONE', *, *, #723, .F. ) ;
#1432=CARTESIAN_POINT ( 'NONE',  ( 0.000000000000000000, 0.000000000000000000, -2.899999999999999911 ) ) ;
#1466=AXIS2_PLACEMENT_3D ( 'NONE', #27737, #29794, #30294 ) ;
#1486=CARTESIAN_POINT ( 'NONE',  ( 0.000000000000000000, 0.000000000000000000, 3.100000000000000533 ) ) ;
#1500=ORIENTED_EDGE ( 'NONE', *, *, #5938, .T. ) ;
#1503=CARTESIAN_POINT ( 'NONE',  ( 0.000000000000000000, 0.000000000000000000, -2.899999999999999911 ) ) ;
#1533=CONICAL_SURFACE ( 'NONE', #9166, 3.499999999999999556, 1.047197551196589638 ) ;
#1544=DIRECTION ( 'NONE',  ( -0.000000000000000000, -0.000000000000000000, -1.000000000000000000 ) ) ;
#1707=DIRECTION ( 'NONE',  ( 1.000000000000000000, 0.000000000000000000, 0.000000000000000000 ) ) ;
#1750=CARTESIAN_POINT ( 'NONE',  ( 1.153701847711638750, 3.375361811986500538, 1.891580053702728746E-15 ) ) ;
#1780=VERTEX_POINT ( 'NONE', #30592 ) ;
#1792=CARTESIAN_POINT ( 'NONE',  ( -3.500000000000000888, 1.362959798491825802, -2.760265505016211041 ) ) ;
#1799=AXIS2_PLACEMENT_3D ( 'NONE', #12760, #28432, #33539 ) ;
#1879=CYLINDRICAL_SURFACE ( 'NONE', #10188, 2.000000000000000888 ) ;
#1882=ORIENTED_EDGE ( 'NONE', *, *, #28419, .T. ) ;
#1899=EDGE_CURVE ( 'NONE', #16312, #19546, #5899, .T. ) ;
#1913=EDGE_LOOP ( 'NONE', ( #27322, #2739, #32652 ) ) ;
#1932=CARTESIAN_POINT ( 'NONE',  ( -3.499999999999999556, -3.004629197474309385E-15, 0.000000000000000000 ) ) ;
#1949=ORIENTED_EDGE ( 'NONE', *, *, #15619, .F. ) ;
#1953=CARTESIAN_POINT ( 'NONE',  ( 1.650000000000000133, 0.000000000000000000, -2.899999999999999911 ) ) ;
#1958=EDGE_LOOP ( 'NONE', ( #3589, #13076, #7075, #26419 ) ) ;
#1962=CARTESIAN_POINT ( 'NONE',  ( 3.500000000000004441, -0.6807265984995719554, -2.870648692803527524 ) ) ;
#2011=CARTESIAN_POINT ( 'NONE',  ( 0.000000000000000000, 0.000000000000000000, 9.480888224575629408 ) ) ;
#2022=CARTESIAN_POINT ( 'NONE',  ( 0.5735064479039687635, -3.710337782248086747, -2.761158938895358350 ) ) ;
#2023=CARTESIAN_POINT ( 'NONE',  ( 3.499999999999993339, -2.020725942163723143, -0.3126073911696551910 ) ) ;
#2031=CARTESIAN_POINT ( 'NONE',  ( 0.000000000000000000, 0.000000000000000000, 0.000000000000000000 ) ) ;
#2056=CARTESIAN_POINT ( 'NONE',  ( 0.000000000000000000, 0.000000000000000000, -2.899999999999999911 ) ) ;
#2113=CARTESIAN_POINT ( 'NONE',  ( -3.214438021527938005, -2.185595227304884425, -0.2174200650117698586 ) ) ;
#2163=DIRECTION ( 'NONE',  ( 1.000000000000000000, 0.000000000000000000, 0.000000000000000000 ) ) ;
#2174=AXIS2_PLACEMENT_3D ( 'NONE', #9350, #3898, #19407 ) ;
#2201=DIRECTION ( 'NONE',  ( 0.8660254037844359321, 0.5000000000000046629, 0.000000000000000000 ) ) ;
#2216=ORIENTED_EDGE ( 'NONE', *, *, #22715, .T. ) ;
#2243=CARTESIAN_POINT ( 'NONE',  ( -2.428571428571428381, 2.974142226500714333E-16, 2.066666666667000385 ) ) ;
#2258=CONICAL_SURFACE ( 'NONE', #6597, 3.499999999999999556, 1.047197551196589638 ) ;
#2295=ORIENTED_EDGE ( 'NONE', *, *, #23532, .T. ) ;
#2364=CARTESIAN_POINT ( 'NONE',  ( 0.2855619784720492826, -3.876582599186272127, -0.2174200650117948386 ) ) ;
#2372=CARTESIAN_POINT ( 'NONE',  ( 0.000000000000000000, 0.000000000000000000, 2.066666666667000385 ) ) ;
#2376=EDGE_LOOP ( 'NONE', ( #24903, #22825, #26963 ) ) ;
#2404=AXIS2_PLACEMENT_3D ( 'NONE', #8872, #11941, #4266 ) ;
#2407=SURFACE_STYLE_FILL_AREA ( #7858 ) ;
#2416=MECHANICAL_DESIGN_GEOMETRIC_PRESENTATION_REPRESENTATION('',(#13299),#21439);
#2471=CARTESIAN_POINT ( 'NONE',  ( -1.156317065392244547, 3.373851915354613595, -0.02993401039713676146 ) ) ;
#2484=B_SPLINE_CURVE_WITH_KNOTS ( 'NONE', 3,
 ( #32960, #20020, #7079, #1962, #10974, #6013 ),
 .UNSPECIFIED., .F., .F.,
 ( 4, 2, 4 ),
 ( 0.003605240635278499518, 0.004627368318297494891, 0.005649496001316489831 ),
 .UNSPECIFIED. ) ;
#2525=EDGE_CURVE ( 'NONE', #13221, #4173, #16269, .T. ) ;
#2541=DIRECTION ( 'NONE',  ( 0.000000000000000000, 0.000000000000000000, -1.000000000000000000 ) ) ;
#2599=VECTOR ( 'NONE', #8286, 1000.000000000000000 ) ;
#2620=AXIS2_PLACEMENT_3D ( 'NONE', #27731, #32498, #4567 ) ;
#2622=FACE_OUTER_BOUND ( 'NONE', #4761, .T. ) ;
#2633=VECTOR ( 'NONE', #33063, 1000.000000000000000 ) ;
#2655=VECTOR ( 'NONE', #29930, 1000.000000000000000 ) ;
#2720=CIRCLE ( 'NONE', #30454, 3.499999999999996003 ) ;
#2739=ORIENTED_EDGE ( 'NONE', *, *, #23532, .F. ) ;
#2770=CARTESIAN_POINT ( 'NONE',  ( 0.000000000000000000, 0.000000000000000000, 0.000000000000000000 ) ) ;
#2919=FACE_OUTER_BOUND ( 'NONE', #7301, .T. ) ;
#2958=EDGE_LOOP ( 'NONE', ( #10194, #3130, #13798 ) ) ;
#2969=VERTEX_POINT ( 'NONE', #25344 ) ;
#2992=B_SPLINE_CURVE_WITH_KNOTS ( 'NONE', 3,
 ( #1353, #30143, #6800, #11575, #1179, #29974 ),
 .UNSPECIFIED., .F., .F.,
 ( 4, 2, 4 ),
 ( 0.002044882221487580483, 0.003063384235218526239, 0.004081886248949471996 ),
 .UNSPECIFIED. ) ;
#3005=DIRECTION ( 'NONE',  ( 1.000000000000000000, 0.000000000000000000, 0.000000000000000000 ) ) ;
#3067=ADVANCED_FACE ( 'NONE', ( #32501 ), #2258, .T. ) ;
#3115=CARTESIAN_POINT ( 'NONE',  ( 1.750000000000014211, 3.031088913245526317, -2.899999999999999911 ) ) ;
#3130=ORIENTED_EDGE ( 'NONE', *, *, #21594, .F. ) ;
#3135=DIRECTION ( 'NONE',  ( -0.000000000000000000, -0.000000000000000000, -1.000000000000000000 ) ) ;
#3145=DIRECTION ( 'NONE',  ( 1.000000000000000000, 0.000000000000000000, 0.000000000000000000 ) ) ;
#3186=AXIS2_PLACEMENT_3D ( 'NONE', #31302, #21229, #5400 ) ;
#3211=ORIENTED_EDGE ( 'NONE', *, *, #18761, .F. ) ;
#3263=DIRECTION ( 'NONE',  ( -0.000000000000000000, -0.000000000000000000, -1.000000000000000000 ) ) ;
#3285=FACE_BOUND ( 'NONE', #4851, .T. ) ;
#3314=EDGE_CURVE ( 'NONE', #10897, #33645, #17856, .T. ) ;
#3430=CIRCLE ( 'NONE', #18161, 2.428571428571428381 ) ;
#3439=EDGE_LOOP ( 'NONE', ( #32526, #8742, #29770 ) ) ;
#3447=CARTESIAN_POINT ( 'NONE',  ( 0.000000000000000000, 0.000000000000000000, 0.000000000000000000 ) ) ;
#3492=LINE ( 'NONE', #13883, #33347 ) ;
#3507=ADVANCED_FACE ( 'NONE', ( #4574 ), #14960, .T. ) ;
#3509=CARTESIAN_POINT ( 'NONE',  ( 3.499999999999996891, 0.000000000000000000, 9.480888224575629408 ) ) ;
#3535=EDGE_LOOP ( 'NONE', ( #12348, #25217, #30285, #15246 ) ) ;
#3589=ORIENTED_EDGE ( 'NONE', *, *, #6380, .F. ) ;
#3675=EDGE_CURVE ( 'NONE', #258, #20656, #18573, .T. ) ;
#3752=ORIENTED_EDGE ( 'NONE', *, *, #13352, .F. ) ;
#3759=CARTESIAN_POINT ( 'NONE',  ( 0.5725525826504702653, 3.710888496608923059, -2.778243469714884117 ) ) ;
#3760=ORIENTED_EDGE ( 'NONE', *, *, #1899, .F. ) ;
#3828=DIRECTION ( 'NONE',  ( -0.000000000000000000, -0.000000000000000000, 1.000000000000000000 ) ) ;
#3864=EDGE_CURVE ( 'NONE', #16396, #33645, #19927, .T. ) ;
#3880=ORIENTED_EDGE ( 'NONE', *, *, #574, .F. ) ;
#3898=DIRECTION ( 'NONE',  ( -0.000000000000000000, -0.000000000000000000, 1.000000000000000000 ) ) ;
#3927=DIRECTION ( 'NONE',  ( 1.000000000000000000, 0.000000000000000000, 0.000000000000000000 ) ) ;
#3943=EDGE_LOOP ( 'NONE', ( #17067, #28863, #22437, #15523, #24825, #17233 ) ) ;
#3964=ADVANCED_FACE ( 'NONE', ( #7052, #17102 ), #4485, .F. ) ;
#3994=ORIENTED_EDGE ( 'NONE', *, *, #574, .T. ) ;
#4009=ORIENTED_EDGE ( 'NONE', *, *, #23927, .T. ) ;
#4084=DIRECTION ( 'NONE',  ( -1.000000000000000000, 0.000000000000000000, 0.000000000000000000 ) ) ;
#4105=LINE ( 'NONE', #1389, #2633 ) ;
#4128=CYLINDRICAL_SURFACE ( 'NONE', #14855, 2.428571428571428381 ) ;
#4140=CARTESIAN_POINT ( 'NONE',  ( -3.500000000000001332, 1.693985822988415046, -0.2182856432892006648 ) ) ;
#4142=DIRECTION ( 'NONE',  ( 1.000000000000000000, 0.000000000000000000, -0.000000000000000000 ) ) ;
#4161=CARTESIAN_POINT ( 'NONE',  ( -1.750000000000014211, 3.031088913245526317, -2.899999999999999911 ) ) ;
#4173=VERTEX_POINT ( 'NONE', #23057 ) ;
#4185=DIRECTION ( 'NONE',  ( -1.000000000000000000, 0.000000000000000000, 0.000000000000000000 ) ) ;
#4257=ORIENTED_EDGE ( 'NONE', *, *, #9759, .T. ) ;
#4263=ORIENTED_EDGE ( 'NONE', *, *, #22410, .T. ) ;
#4265=DIRECTION ( 'NONE',  ( -0.8660254037844362651, 0.5000000000000041078, 0.000000000000000000 ) ) ;
#4266=DIRECTION ( 'NONE',  ( 1.000000000000000000, 0.000000000000000000, 0.000000000000000000 ) ) ;
#4311=EDGE_CURVE ( 'NONE', #29827, #11491, #10949, .T. ) ;
#4317=CARTESIAN_POINT ( 'NONE',  ( -3.499999999999999112, 0.3416723310689463444, 2.286988957586610299E-17 ) ) ;
#4405=DIRECTION ( 'NONE',  ( -1.000000000000000000, 0.000000000000000000, 0.000000000000000000 ) ) ;
#4485=PLANE ( 'NONE',  #31103 ) ;
#4487=DIRECTION ( 'NONE',  ( 0.000000000000000000, 0.000000000000000000, 1.000000000000000000 ) ) ;
#4488=PLANE ( 'NONE',  #9579 ) ;
#4517=CONICAL_SURFACE ( 'NONE', #19736, 3.499999999999999556, 1.047197551196589638 ) ;
#4552=ORIENTED_EDGE ( 'NONE', *, *, #13261, .F. ) ;
#4567=DIRECTION ( 'NONE',  ( -1.000000000000000000, 0.000000000000000000, 0.000000000000000000 ) ) ;
#4574=FACE_OUTER_BOUND ( 'NONE', #24318, .T. ) ;
#4594=EDGE_CURVE ( 'NONE', #5483, #20223, #26450, .T. ) ;
#4605=ORIENTED_EDGE ( 'NONE', *, *, #13314, .T. ) ;
#4661=CARTESIAN_POINT ( 'NONE',  ( -2.343682934607786983, -2.688325911136475899, -0.02993401039715462217 ) ) ;
#4747=AXIS2_PLACEMENT_3D ( 'NONE', #28736, #23782, #3005 ) ;
#4761=EDGE_LOOP ( 'NONE', ( #18178, #16576, #31300, #24192, #4605, #18975 ) ) ;
#4765=ORIENTED_EDGE ( 'NONE', *, *, #24869, .F. ) ;
#4767=TOROIDAL_SURFACE ( 'NONE', #4747, 2.466666666666999408, 1.033333333332998372 ) ;
#4795=VERTEX_POINT ( 'NONE', #32552 ) ;
#4799=DIRECTION ( 'NONE',  ( -0.000000000000000000, -0.000000000000000000, 1.000000000000000000 ) ) ;
#4851=EDGE_LOOP ( 'NONE', ( #7398, #16730 ) ) ;
#4852=CARTESIAN_POINT ( 'NONE',  ( -0.5725525826505220017, -3.710888496608931497, -0.1217565302851259662 ) ) ;
#5005=VERTEX_POINT ( 'NONE', #7859 ) ;
#5097=ORIENTED_EDGE ( 'NONE', *, *, #27929, .T. ) ;
#5176=B_SPLINE_CURVE_WITH_KNOTS ( 'NONE', 3,
 ( #28078, #12577, #30814, #18031, #2364, #12917 ),
 .UNSPECIFIED., .F., .F.,
 ( 4, 2, 4 ),
 ( 0.002044882221487502854, 0.003063384235218504989, 0.004081886248949507558 ),
 .UNSPECIFIED. ) ;
#5200=CARTESIAN_POINT ( 'NONE',  ( 0.000000000000000000, 0.000000000000000000, 2.066666666667000385 ) ) ;
#5211=ADVANCED_FACE ( 'NONE', ( #1172 ), #32176, .T. ) ;
#5241=CARTESIAN_POINT ( 'NONE',  ( -3.499999999999997780, -2.020725942163716038, -2.899999999999999911 ) ) ;
#5395=CARTESIAN_POINT ( 'NONE',  ( 3.500000000000004885, 2.020725942163702715, -0.3126073911696551910 ) ) ;
#5400=DIRECTION ( 'NONE',  ( 1.000000000000000000, 0.000000000000000000, 0.000000000000000000 ) ) ;
#5431=CARTESIAN_POINT ( 'NONE',  ( 0.000000000000000000, 0.000000000000000000, -2.899999999999999911 ) ) ;
#5483=VERTEX_POINT ( 'NONE', #2023 ) ;
#5505=CARTESIAN_POINT ( 'NONE',  ( 2.926493552096022466, 2.351840044243029393, -2.761158938895390325 ) ) ;
#5514=CARTESIAN_POINT ( 'NONE',  ( -1.750000000000014211, 3.031088913245526317, 0.000000000000000000 ) ) ;
#5551=CARTESIAN_POINT ( 'NONE',  ( 0.000000000000000000, 0.000000000000000000, 0.000000000000000000 ) ) ;
#5554=ADVANCED_FACE ( 'NONE', ( #27908 ), #9139, .F. ) ;
#5674=ORIENTED_EDGE ( 'NONE', *, *, #2525, .F. ) ;
#5686=CARTESIAN_POINT ( 'NONE',  ( 0.000000000000000000, 0.000000000000000000, 2.066666666667000385 ) ) ;
#5722=CARTESIAN_POINT ( 'NONE',  ( 0.000000000000000000, 0.000000000000000000, 9.480888224575629408 ) ) ;
#5768=EDGE_CURVE ( 'NONE', #697, #7491, #2484, .T. ) ;
#5798=B_SPLINE_CURVE_WITH_KNOTS ( 'NONE', 3,
 ( #4161, #22226, #9452, #9279, #30237, #12177 ),
 .UNSPECIFIED., .F., .F.,
 ( 4, 2, 4 ),
 ( 0.002044882221487520201, 0.003063384235218497183, 0.004081886248949473731 ),
 .UNSPECIFIED. ) ;
#5831=CARTESIAN_POINT ( 'NONE',  ( 3.500000000000004885, 2.020725942163702715, -2.587392608830344720 ) ) ;
#5832=CARTESIAN_POINT ( 'NONE',  ( 3.500000000000004885, -0.3414694520252363752, -3.023060588750597910E-15 ) ) ;
#5879=ORIENTED_EDGE ( 'NONE', *, *, #31797, .T. ) ;
#5893=( NAMED_UNIT ( * ) PLANE_ANGLE_UNIT ( ) SI_UNIT ( $, .RADIAN. ) );
#5899=CIRCLE ( 'NONE', #26060, 2.466666666666999408 ) ;
#5903=DIRECTION ( 'NONE',  ( 0.000000000000000000, 0.000000000000000000, 1.000000000000000000 ) ) ;
#5938=EDGE_CURVE ( 'NONE', #29827, #8405, #10789, .T. ) ;
#5945=DIRECTION ( 'NONE',  ( 8.584654849926598947E-16, -1.000000000000000000, 0.000000000000000000 ) ) ;
#6007=EDGE_CURVE ( 'NONE', #13631, #13221, #28196, .T. ) ;
#6013=CARTESIAN_POINT ( 'NONE',  ( 3.499999999999999556, 0.000000000000000000, -2.899999999999999911 ) ) ;
#6082=ORIENTED_EDGE ( 'NONE', *, *, #235, .F. ) ;
#6132=CARTESIAN_POINT ( 'NONE',  ( -1.649999999999999911, 2.020667218593133001E-16, 2.066666666667000385 ) ) ;
#6173=DIRECTION ( 'NONE',  ( -0.000000000000000000, -0.000000000000000000, 1.000000000000000000 ) ) ;
#6181=( GEOMETRIC_REPRESENTATION_CONTEXT ( 3 ) GLOBAL_UNCERTAINTY_ASSIGNED_CONTEXT ( ( #16903 ) ) GLOBAL_UNIT_ASSIGNED_CONTEXT ( ( #8959, #19524, #29408 ) ) REPRESENTATION_CONTEXT ( 'NONE', 'WORKASPACE' ) );
#6300=CARTESIAN_POINT ( 'NONE',  ( -2.428571428571428381, 2.974142226500714333E-16, 9.480888224575629408 ) ) ;
#6302=ORIENTED_EDGE ( 'NONE', *, *, #19789, .T. ) ;
#6348=ORIENTED_EDGE ( 'NONE', *, *, #5938, .F. ) ;
#6358=CARTESIAN_POINT ( 'NONE',  ( 1.517883041479706208E-15, 4.041451884327390331, -0.3126073911696551910 ) ) ;
#6361=DIRECTION ( 'NONE',  ( -0.000000000000000000, -0.000000000000000000, 1.000000000000000000 ) ) ;
#6363=AXIS2_PLACEMENT_3D ( 'NONE', #11164, #8600, #24099 ) ;
#6380=EDGE_CURVE ( 'NONE', #23586, #19626, #25692, .T. ) ;
#6434=EDGE_LOOP ( 'NONE', ( #12045, #33040, #21796 ) ) ;
#6572=CARTESIAN_POINT ( 'NONE',  ( -3.499999999999999556, -3.004629197474309385E-15, -2.899999999999999911 ) ) ;
#6574=SURFACE_STYLE_FILL_AREA ( #19184 ) ;
#6597=AXIS2_PLACEMENT_3D ( 'NONE', #1503, #19565, #9853 ) ;
#6668=CARTESIAN_POINT ( 'NONE',  ( -1.750000000000016209, -3.031088913245524985, -2.899999999999999911 ) ) ;
#6682=ADVANCED_FACE ( 'NONE', ( #14415 ), #8627, .F. ) ;
#6692=UNCERTAINTY_MEASURE_WITH_UNIT (LENGTH_MEASURE( 1.000000000000000082E-05 ), #18688, 'distance_accuracy_value', 'NONE');
#6703=AXIS2_PLACEMENT_3D ( 'NONE', #26088, #13133, #23526 ) ;
#6728=DIRECTION ( 'NONE',  ( 0.000000000000000000, 0.000000000000000000, 1.000000000000000000 ) ) ;
#6793=CARTESIAN_POINT ( 'NONE',  ( 0.000000000000000000, 0.000000000000000000, -2.874600000000001376 ) ) ;
#6800=CARTESIAN_POINT ( 'NONE',  ( -2.343682934607786539, -2.688325911136476343, -2.870065989602846201 ) ) ;
#6818=EDGE_CURVE ( 'NONE', #10366, #21724, #28217, .T. ) ;
#6820=B_SPLINE_CURVE_WITH_KNOTS ( 'NONE', 3,
 ( #20503, #23225, #25786, #30905, #28841, #23401 ),
 .UNSPECIFIED., .F., .F.,
 ( 4, 2, 4 ),
 ( 0.005649496001316488963, 0.006672230966438344631, 0.007694965931560200298 ),
 .UNSPECIFIED. ) ;
#6825=PLANE ( 'NONE',  #14537 ) ;
#6886=AXIS2_PLACEMENT_3D ( 'NONE', #3447, #26780, #18625 ) ;
#6913=AXIS2_PLACEMENT_3D ( 'NONE', #21646, #24375, #21311 ) ;
#6928=FACE_OUTER_BOUND ( 'NONE', #33471, .T. ) ;
#6959=B_SPLINE_CURVE_WITH_KNOTS ( 'NONE', 3,
 ( #1072, #29180, #10961, #733, #5832, #21509 ),
 .UNSPECIFIED., .F., .F.,
 ( 4, 2, 4 ),
 ( 0.003605240635278498650, 0.004627368318297494024, 0.005649496001316488963 ),
 .UNSPECIFIED. ) ;
#7009=CARTESIAN_POINT ( 'NONE',  ( 1.750000000000016209, -3.031088913245524985, 0.000000000000000000 ) ) ;
#7052=FACE_BOUND ( 'NONE', #9753, .T. ) ;
#7053=CYLINDRICAL_SURFACE ( 'NONE', #14551, 1.650000000000000133 ) ;
#7059=FACE_OUTER_BOUND ( 'NONE', #2376, .T. ) ;
#7075=ORIENTED_EDGE ( 'NONE', *, *, #17645, .T. ) ;
#7079=CARTESIAN_POINT ( 'NONE',  ( 3.500000000000004885, -1.355464348821719733, -2.761841578728545965 ) ) ;
#7085=CARTESIAN_POINT ( 'NONE',  ( -3.500000000000001332, 1.693985822988442580, -2.681714356710791947 ) ) ;
#7115=ORIENTED_EDGE ( 'NONE', *, *, #13066, .F. ) ;
#7224=ORIENTED_EDGE ( 'NONE', *, *, #16463, .F. ) ;
#7268=STYLED_ITEM ( 'NONE', ( #1302 ), #20158 ) ;
#7301=EDGE_LOOP ( 'NONE', ( #1500, #9879 ) ) ;
#7376=ORIENTED_EDGE ( 'NONE', *, *, #24018, .F. ) ;
#7398=ORIENTED_EDGE ( 'NONE', *, *, #23828, .F. ) ;
#7414=ADVANCED_FACE ( 'NONE', ( #7059 ), #30430, .T. ) ;
#7437=CARTESIAN_POINT ( 'NONE',  ( 2.428571428571428381, 0.000000000000000000, 2.066666666667000385 ) ) ;
#7442=DIRECTION ( 'NONE',  ( -0.000000000000000000, -0.000000000000000000, 1.000000000000000000 ) ) ;
#7486=DIRECTION ( 'NONE',  ( 0.5000000000000046629, -0.8660254037844359321, 0.000000000000000000 ) ) ;
#7491=VERTEX_POINT ( 'NONE', #12332 ) ;
#7541=DIRECTION ( 'NONE',  ( 1.000000000000000000, 0.000000000000000000, 0.000000000000000000 ) ) ;
#7671=CARTESIAN_POINT ( 'NONE',  ( 1.750000000000016209, -3.031088913245524985, 0.000000000000000000 ) ) ;
#7793=ORIENTED_EDGE ( 'NONE', *, *, #31597, .F. ) ;
#7849=CARTESIAN_POINT ( 'NONE',  ( 0.000000000000000000, 0.000000000000000000, -2.899999999999999911 ) ) ;
#7858=FILL_AREA_STYLE ('',( #28801 ) ) ;
#7859=CARTESIAN_POINT ( 'NONE',  ( -2.000000000000000888, 2.449293598294707893E-16, -2.899999999999999911 ) ) ;
#7912=DIRECTION ( 'NONE',  ( 1.000000000000000000, 0.000000000000000000, 0.000000000000000000 ) ) ;
#7984=CARTESIAN_POINT ( 'NONE',  ( -6.830473686658677934E-14, -4.041451884327390331, -0.3126073911696551910 ) ) ;
#8011=ORIENTED_EDGE ( 'NONE', *, *, #10969, .T. ) ;
#8102=CONICAL_SURFACE ( 'NONE', #20049, 3.499999999999999556, 1.047197551196589638 ) ;
#8110=ORIENTED_EDGE ( 'NONE', *, *, #24556, .F. ) ;
#8130=CARTESIAN_POINT ( 'NONE',  ( 2.047034997319582939, 2.859595677584332307, 1.982057096575062005E-15 ) ) ;
#8242=DIRECTION ( 'NONE',  ( 0.000000000000000000, 0.000000000000000000, -1.000000000000000000 ) ) ;
#8286=DIRECTION ( 'NONE',  ( 0.000000000000000000, 0.000000000000000000, 1.000000000000000000 ) ) ;
#8403=CARTESIAN_POINT ( 'NONE',  ( -3.499999999999999556, -0.3414694520252371523, -2.900000000000000355 ) ) ;
#8405=VERTEX_POINT ( 'NONE', #2243 ) ;
#8480=EDGE_LOOP ( 'NONE', ( #18089, #29553, #27544, #23084 ) ) ;
#8535=ORIENTED_EDGE ( 'NONE', *, *, #17294, .T. ) ;
#8570=AXIS2_PLACEMENT_3D ( 'NONE', #22774, #7442, #2163 ) ;
#8600=DIRECTION ( 'NONE',  ( 0.000000000000000000, 0.000000000000000000, 1.000000000000000000 ) ) ;
#8607=AXIS2_PLACEMENT_3D ( 'NONE', #6793, #17181, #4405 ) ;
#8614=CARTESIAN_POINT ( 'NONE',  ( 3.214438021527930012, 2.185595227304852450, -0.2174200650117560363 ) ) ;
#8627=CONICAL_SURFACE ( 'NONE', #27671, 2.000000000000000000, 0.9599310885968733720 ) ;
#8650=ORIENTED_EDGE ( 'NONE', *, *, #28490, .T. ) ;
#8678=DIRECTION ( 'NONE',  ( 0.000000000000000000, 0.000000000000000000, 1.000000000000000000 ) ) ;
#8681=EDGE_CURVE ( 'NONE', #4795, #1780, #2720, .T. ) ;
#8702=EDGE_CURVE ( 'NONE', #9440, #10897, #2992, .T. ) ;
#8742=ORIENTED_EDGE ( 'NONE', *, *, #6007, .F. ) ;
#8750=EDGE_CURVE ( 'NONE', #21724, #10366, #27186, .T. ) ;
#8856=ORIENTED_EDGE ( 'NONE', *, *, #8702, .F. ) ;
#8872=CARTESIAN_POINT ( 'NONE',  ( 0.000000000000000000, 0.000000000000000000, 0.000000000000000000 ) ) ;
#8885=DIRECTION ( 'NONE',  ( -1.000000000000000000, 0.000000000000000000, 0.000000000000000000 ) ) ;
#8910=DIRECTION ( 'NONE',  ( -0.000000000000000000, -0.000000000000000000, 1.000000000000000000 ) ) ;
#8959=( LENGTH_UNIT ( ) NAMED_UNIT ( * ) SI_UNIT ( .MILLI., .METRE. ) );
#9010=CARTESIAN_POINT ( 'NONE',  ( -6.830473686658677934E-14, -4.041451884327390331, -2.587392608830344720 ) ) ;
#9018=CARTESIAN_POINT ( 'NONE',  ( 0.000000000000000000, 0.000000000000000000, 2.066666666666666430 ) ) ;
#9078=ORIENTED_EDGE ( 'NONE', *, *, #33526, .F. ) ;
#9139=CONICAL_SURFACE ( 'NONE', #8607, 2.000000000000000000, 0.9599310885968733720 ) ;
#9166=AXIS2_PLACEMENT_3D ( 'NONE', #23125, #18186, #28240 ) ;
#9176=EDGE_CURVE ( 'NONE', #20223, #258, #27589, .T. ) ;
#9226=CARTESIAN_POINT ( 'NONE',  ( -1.153701847711675166, -3.375361811986517857, -2.899999999999983924 ) ) ;
#9264=CARTESIAN_POINT ( 'NONE',  ( 3.500000000000004441, 0.3416723310689538939, -2.899999999999996803 ) ) ;
#9279=CARTESIAN_POINT ( 'NONE',  ( -0.5735064479039797547, 3.710337782248037009, -2.761158938895385884 ) ) ;
#9282=ORIENTED_EDGE ( 'NONE', *, *, #31597, .T. ) ;
#9292=CARTESIAN_POINT ( 'NONE',  ( -3.500000000000001332, 2.020725942163708488, -2.587392608830344720 ) ) ;
#9350=CARTESIAN_POINT ( 'NONE',  ( 0.000000000000000000, 0.000000000000000000, -2.874600000000001376 ) ) ;
#9360=B_SPLINE_CURVE_WITH_KNOTS ( 'NONE', 3,
 ( #32326, #17161, #19380, #1330 ),
 .UNSPECIFIED., .F., .F.,
 ( 4, 4 ),
 ( 2.380739282314300957E-07, 0.002044882221487520201 ),
 .UNSPECIFIED. ) ;
#9387=CARTESIAN_POINT ( 'NONE',  ( -0.5725525826505220017, -3.710888496608931497, -2.778243469714873903 ) ) ;
#9429=AXIS2_PLACEMENT_3D ( 'NONE', #19437, #3263, #16711 ) ;
#9440=VERTEX_POINT ( 'NONE', #24211 ) ;
#9452=CARTESIAN_POINT ( 'NONE',  ( -1.156317065392243659, 3.373851915354613151, -2.870065989602862633 ) ) ;
#9579=AXIS2_PLACEMENT_3D ( 'NONE', #10302, #10463, #13009 ) ;
#9599=ADVANCED_FACE ( 'NONE', ( #16874 ), #14323, .T. ) ;
#9630=AXIS2_PLACEMENT_3D ( 'NONE', #5431, #18382, #21097 ) ;
#9704=B_SPLINE_CURVE_WITH_KNOTS ( 'NONE', 3,
 ( #19317, #9264, #1428, #16923, #32762, #16759 ),
 .UNSPECIFIED., .F., .F.,
 ( 4, 2, 4 ),
 ( 0.005649496001316489831, 0.006672230966438345498, 0.007694965931560201165 ),
 .UNSPECIFIED. ) ;
#9753=EDGE_LOOP ( 'NONE', ( #9078, #567 ) ) ;
#9759=EDGE_CURVE ( 'NONE', #9440, #13631, #17804, .T. ) ;
#9786=ADVANCED_FACE ( 'NONE', ( #19772 ), #6825, .T. ) ;
#9853=DIRECTION ( 'NONE',  ( 1.000000000000000000, 0.000000000000000000, 0.000000000000000000 ) ) ;
#9879=ORIENTED_EDGE ( 'NONE', *, *, #32900, .T. ) ;
#9886=CARTESIAN_POINT ( 'NONE',  ( 0.000000000000000000, 0.000000000000000000, -25.03750572909317285 ) ) ;
#9999=PRODUCT_DEFINITION_SHAPE ( 'NONE', 'NONE',  #33139 ) ;
#10050=FACE_OUTER_BOUND ( 'NONE', #28933, .T. ) ;
#10062=EDGE_LOOP ( 'NONE', ( #29979, #31502, #3211 ) ) ;
#10081=B_SPLINE_CURVE_WITH_KNOTS ( 'NONE', 3,
 ( #14335, #9387, #9226, #6668 ),
 .UNSPECIFIED., .F., .F.,
 ( 4, 4 ),
 ( 2.380739283024902572E-07, 0.002044882221487580483 ),
 .UNSPECIFIED. ) ;
#10188=AXIS2_PLACEMENT_3D ( 'NONE', #9886, #17205, #22656 ) ;
#10194=ORIENTED_EDGE ( 'NONE', *, *, #16046, .T. ) ;
#10210=AXIS2_PLACEMENT_3D ( 'NONE', #1376, #22152, #1707 ) ;
#10302=CARTESIAN_POINT ( 'NONE',  ( 3.500000000000004885, 2.020725942163676070, -2.899999999999999911 ) ) ;
#10318=AXIS2_PLACEMENT_3D ( 'NONE', #7849, #16001, #31023 ) ;
#10335=DIRECTION ( 'NONE',  ( -0.000000000000000000, -0.000000000000000000, 1.000000000000000000 ) ) ;
#10359=ADVANCED_FACE ( 'NONE', ( #22112 ), #26523, .T. ) ;
#10366=VERTEX_POINT ( 'NONE', #11898 ) ;
#10463=DIRECTION ( 'NONE',  ( -1.000000000000000000, 0.000000000000000000, 0.000000000000000000 ) ) ;
#10486=DIRECTION ( 'NONE',  ( -0.000000000000000000, -0.000000000000000000, 1.000000000000000000 ) ) ;
#10568=DIRECTION ( 'NONE',  ( 0.8191520442889872466, 1.003171929053519200E-16, -0.5735764363510525987 ) ) ;
#10590=ADVANCED_FACE ( 'NONE', ( #13077 ), #17847, .F. ) ;
#10600=B_SPLINE_CURVE_WITH_KNOTS ( 'NONE', 3,
 ( #23702, #4852, #19845, #28017 ),
 .UNSPECIFIED., .F., .F.,
 ( 4, 4 ),
 ( 2.380739283024784782E-07, 0.002044882221487580917 ),
 .UNSPECIFIED. ) ;
#10694=CARTESIAN_POINT ( 'NONE',  ( 0.000000000000000000, 0.000000000000000000, 0.000000000000000000 ) ) ;
#10743=PRESENTATION_STYLE_ASSIGNMENT (( #28468 ) ) ;
#10789=CIRCLE ( 'NONE', #29276, 2.428571428571428381 ) ;
#10793=AXIS2_PLACEMENT_3D ( 'NONE', #29824, #17376, #4084 ) ;
#10897=VERTEX_POINT ( 'NONE', #11022 ) ;
#10922=VERTEX_POINT ( 'NONE', #21402 ) ;
#10949=LINE ( 'NONE', #19110, #21308 ) ;
#10961=CARTESIAN_POINT ( 'NONE',  ( 3.500000000000004885, -1.355464348821720177, -0.1381584212714541127 ) ) ;
#10969=EDGE_CURVE ( 'NONE', #32873, #17505, #12113, .T. ) ;
#10974=CARTESIAN_POINT ( 'NONE',  ( 3.500000000000004885, -0.3414694520252361531, -2.899999999999997247 ) ) ;
#11022=CARTESIAN_POINT ( 'NONE',  ( -3.499999999999997780, -2.020725942163714262, -2.587392608830344720 ) ) ;
#11046=CARTESIAN_POINT ( 'NONE',  ( 2.385244779468109755E-15, 4.041451884327391220, -2.587392608830344720 ) ) ;
#11085=CIRCLE ( 'NONE', #22479, 3.499999999999996003 ) ;
#11164=CARTESIAN_POINT ( 'NONE',  ( 0.000000000000000000, 0.000000000000000000, 0.000000000000000000 ) ) ;
#11177=ORIENTED_EDGE ( 'NONE', *, *, #28713, .F. ) ;
#11253=CIRCLE ( 'NONE', #12321, 3.500000000000000444 ) ;
#11259=DIRECTION ( 'NONE',  ( -1.000000000000000000, 0.000000000000000000, 0.000000000000000000 ) ) ;
#11340=ORIENTED_EDGE ( 'NONE', *, *, #9176, .T. ) ;
#11364=CARTESIAN_POINT ( 'NONE',  ( -3.499999999999999556, -0.3414694520252377630, -3.134021904840910022E-17 ) ) ;
#11395=ORIENTED_EDGE ( 'NONE', *, *, #1334, .T. ) ;
#11429=CARTESIAN_POINT ( 'NONE',  ( 1.153701847711638750, 3.375361811986500538, -2.900000000000002132 ) ) ;
#11491=VERTEX_POINT ( 'NONE', #29667 ) ;
#11515=FACE_OUTER_BOUND ( 'NONE', #8480, .T. ) ;
#11519=CARTESIAN_POINT ( 'NONE',  ( -3.499999999999999112, 0.3416723310689526172, -2.899999999999999467 ) ) ;
#11575=CARTESIAN_POINT ( 'NONE',  ( -2.926493552096032680, -2.351840044243060923, -2.761158938895374337 ) ) ;
#11593=EDGE_CURVE ( 'NONE', #5005, #2969, #728, .T. ) ;
#11662=DIRECTION ( 'NONE',  ( -0.000000000000000000, -0.000000000000000000, 1.000000000000000000 ) ) ;
#11677=ORIENTED_EDGE ( 'NONE', *, *, #24757, .T. ) ;
#11691=CARTESIAN_POINT ( 'NONE',  ( -3.499999999999999112, 0.6879904500768373454, -2.869836757075878708 ) ) ;
#11719=CARTESIAN_POINT ( 'NONE',  ( 1.750000000000012879, 3.031088913245524097, 1.502314598737187430E-15 ) ) ;
#11772=CLOSED_SHELL ( 'NONE', ( #18079, #27087, #21142, #22058, #6682, #26397, #27829, #33652, #9786, #21999, #32866, #3507, #5211, #3964, #3067, #32908, #15630, #21251, #7414, #29482, #24072, #24988, #10359, #32698, #25918, #19539, #5554, #446, #16648, #10590, #18101, #24098, #9599 ) ) ;
#11801=EDGE_CURVE ( 'NONE', #17505, #15312, #24728, .T. ) ;
#11815=APPLICATION_CONTEXT ( 'automotive_design' ) ;
#11892=VECTOR ( 'NONE', #28425, 1000.000000000000000 ) ;
#11898=CARTESIAN_POINT ( 'NONE',  ( 2.000000000000000000, 2.449293598294706414E-16, -2.874600000000001376 ) ) ;
#11941=DIRECTION ( 'NONE',  ( 0.000000000000000000, 0.000000000000000000, 1.000000000000000000 ) ) ;
#11947=CARTESIAN_POINT ( 'NONE',  ( -1.750000000000014211, 3.031088913245526317, 0.000000000000000000 ) ) ;
#11952=CARTESIAN_POINT ( 'NONE',  ( 2.346298152288388561, -2.686816014504594730, -1.834956978294293449E-14 ) ) ;
#12025=DIRECTION ( 'NONE',  ( 0.000000000000000000, 0.000000000000000000, -1.000000000000000000 ) ) ;
#12045=ORIENTED_EDGE ( 'NONE', *, *, #8702, .T. ) ;
#12094=PRODUCT_DEFINITION_FORMATION_WITH_SPECIFIED_SOURCE ( 'ANY', '', #14029, .NOT_KNOWN. ) ;
#12104=DIRECTION ( 'NONE',  ( 0.5000000000000041078, 0.8660254037844362651, -0.000000000000000000 ) ) ;
#12113=B_SPLINE_CURVE_WITH_KNOTS ( 'NONE', 3,
 ( #1932, #4317, #27648, #32931, #4140, #14702 ),
 .UNSPECIFIED., .F., .F.,
 ( 4, 2, 4 ),
 ( 0.005649496001316481157, 0.006672230966438324681, 0.007694965931560168206 ),
 .UNSPECIFIED. ) ;
#12170=ORIENTED_EDGE ( 'NONE', *, *, #15990, .F. ) ;
#12177=CARTESIAN_POINT ( 'NONE',  ( 2.385244779468109755E-15, 4.041451884327391220, -2.587392608830344720 ) ) ;
#12188=CARTESIAN_POINT ( 'NONE',  ( 3.500000000000004885, 2.020725942163702715, -2.587392608830344720 ) ) ;
#12198=CARTESIAN_POINT ( 'NONE',  ( 0.000000000000000000, 0.000000000000000000, -2.874600000000001376 ) ) ;
#12213=LINE ( 'NONE', #25152, #14008 ) ;
#12239=CARTESIAN_POINT ( 'NONE',  ( 1.156317065392246990, -3.373851915354654007, -2.870065989602839984 ) ) ;
#12321=AXIS2_PLACEMENT_3D ( 'NONE', #10694, #15960, #28587 ) ;
#12332=CARTESIAN_POINT ( 'NONE',  ( 3.499999999999999556, 0.000000000000000000, -2.899999999999999911 ) ) ;
#12348=ORIENTED_EDGE ( 'NONE', *, *, #32900, .F. ) ;
#12411=CARTESIAN_POINT ( 'NONE',  ( 0.2855619784720492826, -3.876582599186272571, -2.682579934988205128 ) ) ;
#12519=EDGE_CURVE ( 'NONE', #10922, #9440, #10081, .T. ) ;
#12555=MANIFOLD_SOLID_BREP ( 'TorqueElement', #11772 ) ;
#12577=CARTESIAN_POINT ( 'NONE',  ( 1.452965002680450812, -3.202582148906760739, -1.877999099004871997E-14 ) ) ;
#12583=CARTESIAN_POINT ( 'NONE',  ( -3.500000000000001332, 2.020725942163708488, -2.587392608830344720 ) ) ;
#12587=EDGE_LOOP ( 'NONE', ( #4765, #6348, #27801, #25616 ) ) ;
#12693=AXIS2_PLACEMENT_3D ( 'NONE', #16232, #8242, #16393 ) ;
#12749=DIRECTION ( 'NONE',  ( 0.000000000000000000, 0.000000000000000000, 1.000000000000000000 ) ) ;
#12760=CARTESIAN_POINT ( 'NONE',  ( 0.000000000000000000, 0.000000000000000000, -2.899999999999999911 ) ) ;
#12819=EDGE_LOOP ( 'NONE', ( #7224, #18965 ) ) ;
#12844=ORIENTED_EDGE ( 'NONE', *, *, #3675, .F. ) ;
#12917=CARTESIAN_POINT ( 'NONE',  ( -6.830473686658677934E-14, -4.041451884327390331, -0.3126073911696551910 ) ) ;
#13009=DIRECTION ( 'NONE',  ( 0.000000000000000000, 0.000000000000000000, 1.000000000000000000 ) ) ;
#13066=EDGE_CURVE ( 'NONE', #15536, #10922, #20628, .T. ) ;
#13076=ORIENTED_EDGE ( 'NONE', *, *, #28058, .F. ) ;
#13077=FACE_OUTER_BOUND ( 'NONE', #12587, .T. ) ;
#13115=B_SPLINE_CURVE_WITH_KNOTS ( 'NONE', 3,
 ( #6572, #11519, #11691, #1792, #7085, #9292 ),
 .UNSPECIFIED., .F., .F.,
 ( 4, 2, 4 ),
 ( 0.005649496001316482025, 0.006672230966438342029, 0.007694965931560201165 ),
 .UNSPECIFIED. ) ;
#13133=DIRECTION ( 'NONE',  ( -0.000000000000000000, -0.000000000000000000, 1.000000000000000000 ) ) ;
#13137=ORIENTED_EDGE ( 'NONE', *, *, #15619, .T. ) ;
#13178=LINE ( 'NONE', #243, #18648 ) ;
#13221=VERTEX_POINT ( 'NONE', #17691 ) ;
#13261=EDGE_CURVE ( 'NONE', #20223, #13276, #5176, .T. ) ;
#13276=VERTEX_POINT ( 'NONE', #7984 ) ;
#13299=STYLED_ITEM ( 'NONE', ( #10743 ), #12555 ) ;
#13314=EDGE_CURVE ( 'NONE', #26705, #24119, #13409, .T. ) ;
#13352=EDGE_CURVE ( 'NONE', #33645, #32873, #31188, .T. ) ;
#13356=ORIENTED_EDGE ( 'NONE', *, *, #4594, .F. ) ;
#13359=DIRECTION ( 'NONE',  ( 1.000000000000000000, 0.000000000000000000, 0.000000000000000000 ) ) ;
#13385=FACE_OUTER_BOUND ( 'NONE', #24454, .T. ) ;
#13409=LINE ( 'NONE', #19028, #16021 ) ;
#13412=DIRECTION ( 'NONE',  ( 1.000000000000000000, 0.000000000000000000, 0.000000000000000000 ) ) ;
#13457=AXIS2_PLACEMENT_3D ( 'NONE', #31759, #10335, #15757 ) ;
#13473=DIRECTION ( 'NONE',  ( 0.000000000000000000, 0.000000000000000000, 1.000000000000000000 ) ) ;
#13481=VECTOR ( 'NONE', #8678, 1000.000000000000000 ) ;
#13516=CARTESIAN_POINT ( 'NONE',  ( -0.5735064479039806429, 3.710337782248036120, -0.1388410611046141385 ) ) ;
#13527=DIRECTION ( 'NONE',  ( -0.5000000000000041078, 0.8660254037844362651, 0.000000000000000000 ) ) ;
#13536=ORIENTED_EDGE ( 'NONE', *, *, #13314, .F. ) ;
#13551=DIRECTION ( 'NONE',  ( 1.000000000000000000, 0.000000000000000000, 0.000000000000000000 ) ) ;
#13570=LINE ( 'NONE', #3509, #18922 ) ;
#13631=VERTEX_POINT ( 'NONE', #21909 ) ;
#13647=VECTOR ( 'NONE', #12749, 1000.000000000000000 ) ;
#13662=EDGE_LOOP ( 'NONE', ( #32285, #285, #4009, #19969 ) ) ;
#13665=CARTESIAN_POINT ( 'NONE',  ( 2.047034997319582939, 2.859595677584332307, -2.900000000000001688 ) ) ;
#13670=FACE_OUTER_BOUND ( 'NONE', #20524, .T. ) ;
#13714=CARTESIAN_POINT ( 'NONE',  ( 2.926493552096022466, 2.351840044243029393, -0.1388410611046095033 ) ) ;
#13765=CIRCLE ( 'NONE', #6703, 2.428571428571428381 ) ;
#13798=ORIENTED_EDGE ( 'NONE', *, *, #27251, .T. ) ;
#13832=DIRECTION ( 'NONE',  ( -0.000000000000000000, -0.000000000000000000, 1.000000000000000000 ) ) ;
#13847=CYLINDRICAL_SURFACE ( 'NONE', #16473, 3.499999999999996891 ) ;
#13883=CARTESIAN_POINT ( 'NONE',  ( -2.000000000000000888, 2.449293598294707893E-16, -25.03750572909317285 ) ) ;
#13895=ORIENTED_EDGE ( 'NONE', *, *, #1899, .T. ) ;
#13975=CARTESIAN_POINT ( 'NONE',  ( 0.000000000000000000, 0.000000000000000000, -2.629527361626598836 ) ) ;
#14008=VECTOR ( 'NONE', #17828, 1000.000000000000000 ) ;
#14029=PRODUCT ( 'torque nut 01_iso_ISO 7040-M4-N', 'torque nut 01_iso_ISO 7040-M4-N', '', ( #15677 ) ) ;
#14030=AXIS2_PLACEMENT_3D ( 'NONE', #23866, #13473, #31701 ) ;
#14056=EDGE_LOOP ( 'NONE', ( #28491, #2295, #25672, #4257, #31042, #18339 ) ) ;
#14081=CARTESIAN_POINT ( 'NONE',  ( 0.000000000000000000, 0.000000000000000000, -2.899999999999999911 ) ) ;
#14129=DIRECTION ( 'NONE',  ( 1.000000000000000000, 0.000000000000000000, 0.000000000000000000 ) ) ;
#14309=FACE_OUTER_BOUND ( 'NONE', #30119, .T. ) ;
#14323=CYLINDRICAL_SURFACE ( 'NONE', #10210, 3.499999999999996891 ) ;
#14335=CARTESIAN_POINT ( 'NONE',  ( -6.830473686658677934E-14, -4.041451884327390331, -2.587392608830344720 ) ) ;
#14364=FACE_OUTER_BOUND ( 'NONE', #3535, .T. ) ;
#14415=FACE_OUTER_BOUND ( 'NONE', #24442, .T. ) ;
#14537=AXIS2_PLACEMENT_3D ( 'NONE', #17210, #12104, #4265 ) ;
#14540=CONICAL_SURFACE ( 'NONE', #946, 3.499999999999999556, 1.047197551196589638 ) ;
#14551=AXIS2_PLACEMENT_3D ( 'NONE', #17434, #4487, #25272 ) ;
#14565=VERTEX_POINT ( 'NONE', #26592 ) ;
#14596=CYLINDRICAL_SURFACE ( 'NONE', #8570, 2.000000000000000888 ) ;
#14702=CARTESIAN_POINT ( 'NONE',  ( -3.500000000000001332, 2.020725942163676070, -0.3126073911696459207 ) ) ;
#14706=FACE_OUTER_BOUND ( 'NONE', #1958, .T. ) ;
#14789=CARTESIAN_POINT ( 'NONE',  ( 1.452965002680449924, -3.202582148906760739, -2.899999999999980815 ) ) ;
#14855=AXIS2_PLACEMENT_3D ( 'NONE', #5722, #29869, #24921 ) ;
#14892=AXIS2_PLACEMENT_3D ( 'NONE', #1090, #16580, #13359 ) ;
#14960=PLANE ( 'NONE',  #22353 ) ;
#15022=DIRECTION ( 'NONE',  ( 0.000000000000000000, 0.000000000000000000, -1.000000000000000000 ) ) ;
#15057=ORIENTED_EDGE ( 'NONE', *, *, #12519, .F. ) ;
#15084=CIRCLE ( 'NONE', #13457, 3.499999999999999556 ) ;
#15151=ORIENTED_EDGE ( 'NONE', *, *, #29706, .T. ) ;
#15244=EDGE_LOOP ( 'NONE', ( #13895, #5879 ) ) ;
#15246=ORIENTED_EDGE ( 'NONE', *, *, #4311, .F. ) ;
#15312=VERTEX_POINT ( 'NONE', #25992 ) ;
#15345=( LENGTH_UNIT ( ) NAMED_UNIT ( * ) SI_UNIT ( .MILLI., .METRE. ) );
#15372=VECTOR ( 'NONE', #6728, 1000.000000000000000 ) ;
#15504=ORIENTED_EDGE ( 'NONE', *, *, #24130, .T. ) ;
#15513=( NAMED_UNIT ( * ) PLANE_ANGLE_UNIT ( ) SI_UNIT ( $, .RADIAN. ) );
#15523=ORIENTED_EDGE ( 'NONE', *, *, #24130, .F. ) ;
#15536=VERTEX_POINT ( 'NONE', #1272 ) ;
#15619=EDGE_CURVE ( 'NONE', #10922, #13276, #13178, .T. ) ;
#15623=EDGE_LOOP ( 'NONE', ( #371, #17779, #9282, #11340, #11395, #33214 ) ) ;
#15630=ADVANCED_FACE ( 'NONE', ( #31248 ), #4517, .T. ) ;
#15644=FACE_OUTER_BOUND ( 'NONE', #20476, .T. ) ;
#15677=PRODUCT_CONTEXT ( 'NONE', #20073, 'mechanical' ) ;
#15737=AXIS2_PLACEMENT_3D ( 'NONE', #1432, #11662, #19492 ) ;
#15757=DIRECTION ( 'NONE',  ( 1.000000000000000000, 0.000000000000000000, 0.000000000000000000 ) ) ;
#15786=UNCERTAINTY_MEASURE_WITH_UNIT (LENGTH_MEASURE( 1.000000000000000082E-05 ), #15345, 'distance_accuracy_value', 'NONE');
#15890=ORIENTED_EDGE ( 'NONE', *, *, #23927, .F. ) ;
#15894=CARTESIAN_POINT ( 'NONE',  ( 3.214438021527930012, 2.185595227304852450, -2.682579934988243764 ) ) ;
#15960=DIRECTION ( 'NONE',  ( 0.000000000000000000, 0.000000000000000000, 1.000000000000000000 ) ) ;
#15977=AXIS2_PLACEMENT_3D ( 'NONE', #201, #4799, #7541 ) ;
#15990=EDGE_CURVE ( 'NONE', #10897, #13631, #25813, .T. ) ;
#16001=DIRECTION ( 'NONE',  ( -0.000000000000000000, -0.000000000000000000, -1.000000000000000000 ) ) ;
#16021=VECTOR ( 'NONE', #5903, 1000.000000000000000 ) ;
#16046=EDGE_CURVE ( 'NONE', #4173, #26705, #30707, .T. ) ;
#16105=CARTESIAN_POINT ( 'NONE',  ( 1.525316667890869448E-15, 4.041451884327390331, -2.899999999999999911 ) ) ;
#16127=CARTESIAN_POINT ( 'NONE',  ( -3.499999999999997780, -2.020725942163714262, -0.3126073911696551910 ) ) ;
#16145=EDGE_LOOP ( 'NONE', ( #15504, #19296, #25808, #13536, #5, #25844 ) ) ;
#16171=LINE ( 'NONE', #21787, #13481 ) ;
#16214=DIRECTION ( 'NONE',  ( -0.000000000000000000, -0.000000000000000000, 1.000000000000000000 ) ) ;
#16232=CARTESIAN_POINT ( 'NONE',  ( 0.000000000000000000, 2.428571428571428381, 3.099999999999999645 ) ) ;
#16251=DIRECTION ( 'NONE',  ( -0.8660254037844362651, -0.5000000000000041078, 0.000000000000000000 ) ) ;
#16269=CIRCLE ( 'NONE', #10318, 3.499999999999999556 ) ;
#16279=CARTESIAN_POINT ( 'NONE',  ( 1.750000000000012879, 3.031088913245524097, 1.502314598737187430E-15 ) ) ;
#16312=VERTEX_POINT ( 'NONE', #30020 ) ;
#16366=DIRECTION ( 'NONE',  ( -0.000000000000000000, -0.000000000000000000, 1.000000000000000000 ) ) ;
#16387=CARTESIAN_POINT ( 'NONE',  ( -3.499999999999999556, -0.6807265984995714003, -2.870648692803531077 ) ) ;
#16393=DIRECTION ( 'NONE',  ( -1.000000000000000000, 0.000000000000000000, -0.000000000000000000 ) ) ;
#16396=VERTEX_POINT ( 'NONE', #25748 ) ;
#16463=EDGE_CURVE ( 'NONE', #22313, #19626, #31755, .T. ) ;
#16473=AXIS2_PLACEMENT_3D ( 'NONE', #24577, #6173, #31576 ) ;
#16519=CARTESIAN_POINT ( 'NONE',  ( 0.000000000000000000, 1.649999999999999911, 2.066666666667000385 ) ) ;
#16576=ORIENTED_EDGE ( 'NONE', *, *, #28419, .F. ) ;
#16580=DIRECTION ( 'NONE',  ( -0.000000000000000000, -0.000000000000000000, -1.000000000000000000 ) ) ;
#16648=ADVANCED_FACE ( 'NONE', ( #24361, #2919 ), #31694, .F. ) ;
#16711=DIRECTION ( 'NONE',  ( 1.000000000000000000, 0.000000000000000000, 0.000000000000000000 ) ) ;
#16728=AXIS2_PLACEMENT_3D ( 'NONE', #1486, #17488, #20393 ) ;
#16730=ORIENTED_EDGE ( 'NONE', *, *, #32029, .F. ) ;
#16759=CARTESIAN_POINT ( 'NONE',  ( 3.500000000000004885, 2.020725942163702715, -2.587392608830344720 ) ) ;
#16874=FACE_OUTER_BOUND ( 'NONE', #15623, .T. ) ;
#16903=UNCERTAINTY_MEASURE_WITH_UNIT (LENGTH_MEASURE( 1.000000000000000082E-05 ), #8959, 'distance_accuracy_value', 'NONE');
#16923=CARTESIAN_POINT ( 'NONE',  ( 3.500000000000004441, 1.362959798491822250, -2.760265505016209264 ) ) ;
#17053=AXIS2_PLACEMENT_3D ( 'NONE', #2031, #2541, #23151 ) ;
#17067=ORIENTED_EDGE ( 'NONE', *, *, #28713, .T. ) ;
#17072=AXIS2_PLACEMENT_3D ( 'NONE', #16519, #31856, #21300 ) ;
#17100=EDGE_CURVE ( 'NONE', #19626, #22313, #24632, .T. ) ;
#17102=FACE_OUTER_BOUND ( 'NONE', #14056, .T. ) ;
#17161=CARTESIAN_POINT ( 'NONE',  ( -2.927447417349532177, 2.351289329882143786, -2.778243469714890779 ) ) ;
#17181=DIRECTION ( 'NONE',  ( 0.000000000000000000, 0.000000000000000000, -1.000000000000000000 ) ) ;
#17191=ORIENTED_EDGE ( 'NONE', *, *, #11801, .F. ) ;
#17205=DIRECTION ( 'NONE',  ( -0.000000000000000000, -0.000000000000000000, 1.000000000000000000 ) ) ;
#17210=CARTESIAN_POINT ( 'NONE',  ( 3.500000000000004885, 2.020725942163676070, -2.899999999999999911 ) ) ;
#17233=ORIENTED_EDGE ( 'NONE', *, *, #25637, .F. ) ;
#17262=CARTESIAN_POINT ( 'NONE',  ( -1.750000000000016209, -3.031088913245524985, 0.000000000000000000 ) ) ;
#17294=EDGE_CURVE ( 'NONE', #5005, #21724, #3492, .T. ) ;
#17376=DIRECTION ( 'NONE',  ( 0.000000000000000000, 0.000000000000000000, -1.000000000000000000 ) ) ;
#17433=DIRECTION ( 'NONE',  ( 0.000000000000000000, 0.000000000000000000, 1.000000000000000000 ) ) ;
#17434=CARTESIAN_POINT ( 'NONE',  ( 0.000000000000000000, 0.000000000000000000, -2.899999999999999911 ) ) ;
#17478=LINE ( 'NONE', #21912, #2655 ) ;
#17488=DIRECTION ( 'NONE',  ( -0.000000000000000000, -0.000000000000000000, 1.000000000000000000 ) ) ;
#17505=VERTEX_POINT ( 'NONE', #30235 ) ;
#17557=CARTESIAN_POINT ( 'NONE',  ( -2.927447417349541059, 2.351289329882138457, -0.1217565302851113529 ) ) ;
#17562=CARTESIAN_POINT ( 'NONE',  ( 3.499999999999993339, -2.020725942163723143, -0.3126073911696551910 ) ) ;
#17564=LINE ( 'NONE', #25234, #18930 ) ;
#17604=CARTESIAN_POINT ( 'NONE',  ( -2.926493552096033124, -2.351840044243060035, -0.1388410611046252408 ) ) ;
#17645=EDGE_CURVE ( 'NONE', #21522, #22313, #30062, .T. ) ;
#17686=DIRECTION ( 'NONE',  ( -0.5000000000000046629, -0.8660254037844359321, 0.000000000000000000 ) ) ;
#17691=CARTESIAN_POINT ( 'NONE',  ( -1.750000000000014211, 3.031088913245526317, -2.899999999999999911 ) ) ;
#17719=FACE_OUTER_BOUND ( 'NONE', #13662, .T. ) ;
#17730=CARTESIAN_POINT ( 'NONE',  ( -3.500000000000001332, 2.020725942163676070, -0.3126073911696459207 ) ) ;
#17779=ORIENTED_EDGE ( 'NONE', *, *, #235, .T. ) ;
#17793=AXIS2_PLACEMENT_3D ( 'NONE', #5200, #23433, #3145 ) ;
#17804=CIRCLE ( 'NONE', #22145, 3.499999999999999556 ) ;
#17827=CIRCLE ( 'NONE', #14030, 3.500000000000000444 ) ;
#17828=DIRECTION ( 'NONE',  ( -0.000000000000000000, -0.000000000000000000, 1.000000000000000000 ) ) ;
#17847=CYLINDRICAL_SURFACE ( 'NONE', #29790, 2.428571428571428381 ) ;
#17856=LINE ( 'NONE', #25715, #13647 ) ;
#17965=DIRECTION ( 'NONE',  ( 0.000000000000000000, 0.000000000000000000, 1.000000000000000000 ) ) ;
#18031=CARTESIAN_POINT ( 'NONE',  ( 0.5735064479039692076, -3.710337782248087191, -0.1388410611046418386 ) ) ;
#18038=DIRECTION ( 'NONE',  ( 1.000000000000000000, 0.000000000000000000, 0.000000000000000000 ) ) ;
#18079=ADVANCED_FACE ( 'NONE', ( #13670 ), #13847, .T. ) ;
#18089=ORIENTED_EDGE ( 'NONE', *, *, #19742, .F. ) ;
#18101=ADVANCED_FACE ( 'NONE', ( #3285, #570 ), #24067, .F. ) ;
#18161=AXIS2_PLACEMENT_3D ( 'NONE', #2372, #20249, #18038 ) ;
#18176=AXIS2_PLACEMENT_3D ( 'NONE', #13975, #27258, #11259 ) ;
#18178=ORIENTED_EDGE ( 'NONE', *, *, #22410, .F. ) ;
#18186=DIRECTION ( 'NONE',  ( 0.000000000000000000, 0.000000000000000000, -1.000000000000000000 ) ) ;
#18221=ORIENTED_EDGE ( 'NONE', *, *, #3675, .T. ) ;
#18339=ORIENTED_EDGE ( 'NONE', *, *, #2525, .T. ) ;
#18343=CARTESIAN_POINT ( 'NONE',  ( 3.500000000000004885, 2.020725942163702715, -0.3126073911696551910 ) ) ;
#18382=DIRECTION ( 'NONE',  ( -0.000000000000000000, -0.000000000000000000, -1.000000000000000000 ) ) ;
#18422=AXIS2_PLACEMENT_3D ( 'NONE', #12198, #22585, #32971 ) ;
#18531=AXIS2_PLACEMENT_3D ( 'NONE', #31841, #26559, #5945 ) ;
#18573=CIRCLE ( 'NONE', #31086, 3.499999999999999556 ) ;
#18625=DIRECTION ( 'NONE',  ( 1.000000000000000000, 0.000000000000000000, 0.000000000000000000 ) ) ;
#18648=VECTOR ( 'NONE', #17965, 1000.000000000000000 ) ;
#18688=( LENGTH_UNIT ( ) NAMED_UNIT ( * ) SI_UNIT ( .MILLI., .METRE. ) );
#18704=AXIS2_PLACEMENT_3D ( 'NONE', #2770, #20481, #20982 ) ;
#18761=EDGE_CURVE ( 'NONE', #15312, #20612, #30867, .T. ) ;
#18837=ORIENTED_EDGE ( 'NONE', *, *, #28058, .T. ) ;
#18877=AXIS2_PLACEMENT_3D ( 'NONE', #27009, #29737, #24630 ) ;
#18883=CARTESIAN_POINT ( 'NONE',  ( 3.499999999999993339, -2.020725942163723143, -2.587392608830344720 ) ) ;
#18922=VECTOR ( 'NONE', #32123, 1000.000000000000000 ) ;
#18930=VECTOR ( 'NONE', #25065, 1000.000000000000000 ) ;
#18947=CARTESIAN_POINT ( 'NONE',  ( 0.000000000000000000, 0.000000000000000000, -2.629527361626598836 ) ) ;
#18965=ORIENTED_EDGE ( 'NONE', *, *, #17100, .F. ) ;
#18974=DIRECTION ( 'NONE',  ( 1.000000000000000000, 0.000000000000000000, 0.000000000000000000 ) ) ;
#18975=ORIENTED_EDGE ( 'NONE', *, *, #27929, .F. ) ;
#19020=SURFACE_SIDE_STYLE ('',( #6574 ) ) ;
#19028=CARTESIAN_POINT ( 'NONE',  ( 3.500000000000004885, 2.020725942163676070, -2.899999999999999911 ) ) ;
#19090=CARTESIAN_POINT ( 'NONE',  ( 2.385244779468109755E-15, 4.041451884327391220, -2.587392608830344720 ) ) ;
#19110=CARTESIAN_POINT ( 'NONE',  ( 2.428571428571428381, 0.000000000000000000, 9.480888224575629408 ) ) ;
#19177=CYLINDRICAL_SURFACE ( 'NONE', #18877, 1.650000000000000133 ) ;
#19184=FILL_AREA_STYLE ('',( #19687 ) ) ;
#19189=AXIS2_PLACEMENT_3D ( 'NONE', #20915, #33523, #23468 ) ;
#19296=ORIENTED_EDGE ( 'NONE', *, *, #30827, .T. ) ;
#19303=DIRECTION ( 'NONE',  ( 1.000000000000000000, 0.000000000000000000, 0.000000000000000000 ) ) ;
#19317=CARTESIAN_POINT ( 'NONE',  ( 3.499999999999999556, 0.000000000000000000, -2.899999999999999911 ) ) ;
#19380=CARTESIAN_POINT ( 'NONE',  ( -2.346298152288376571, 2.686816014504558758, -2.900000000000002576 ) ) ;
#19407=DIRECTION ( 'NONE',  ( 1.000000000000000000, 0.000000000000000000, 0.000000000000000000 ) ) ;
#19416=TOROIDAL_SURFACE ( 'NONE', #17793, 2.466666666666999408, 1.033333333332998372 ) ;
#19417=ORIENTED_EDGE ( 'NONE', *, *, #1423, .F. ) ;
#19437=CARTESIAN_POINT ( 'NONE',  ( 0.000000000000000000, 0.000000000000000000, -2.899999999999999911 ) ) ;
#19492=DIRECTION ( 'NONE',  ( 1.000000000000000000, 0.000000000000000000, 0.000000000000000000 ) ) ;
#19524=( NAMED_UNIT ( * ) PLANE_ANGLE_UNIT ( ) SI_UNIT ( $, .RADIAN. ) );
#19539=ADVANCED_FACE ( 'NONE', ( #23541 ), #29035, .T. ) ;
#19546=VERTEX_POINT ( 'NONE', #30885 ) ;
#19562=ORIENTED_EDGE ( 'NONE', *, *, #27047, .T. ) ;
#19565=DIRECTION ( 'NONE',  ( -0.000000000000000000, -0.000000000000000000, 1.000000000000000000 ) ) ;
#19626=VERTEX_POINT ( 'NONE', #6132 ) ;
#19687=FILL_AREA_STYLE_COLOUR ( '', #23047 ) ;
#19701=( GEOMETRIC_REPRESENTATION_CONTEXT ( 3 ) GLOBAL_UNCERTAINTY_ASSIGNED_CONTEXT ( ( #6692 ) ) GLOBAL_UNIT_ASSIGNED_CONTEXT ( ( #18688, #5893, #21237 ) ) REPRESENTATION_CONTEXT ( 'NONE', 'WORKASPACE' ) );
#19718=CARTESIAN_POINT ( 'NONE',  ( 1.517883041479706208E-15, 4.041451884327390331, -0.3126073911696551910 ) ) ;
#19736=AXIS2_PLACEMENT_3D ( 'NONE', #21012, #33292, #7912 ) ;
#19742=EDGE_CURVE ( 'NONE', #23586, #21522, #33422, .T. ) ;
#19772=FACE_OUTER_BOUND ( 'NONE', #16145, .T. ) ;
#19789=EDGE_CURVE ( 'NONE', #23693, #4173, #23169, .T. ) ;
#19823=CARTESIAN_POINT ( 'NONE',  ( -2.047034997319599814, -2.859595677584358953, -1.683223872783745003E-14 ) ) ;
#19845=CARTESIAN_POINT ( 'NONE',  ( -1.153701847711675610, -3.375361811986517413, -1.643114763111695053E-14 ) ) ;
#19922=B_SPLINE_CURVE_WITH_KNOTS ( 'NONE', 3,
 ( #16279, #8130, #31943, #13714, #8614, #18343 ),
 .UNSPECIFIED., .F., .F.,
 ( 4, 2, 4 ),
 ( 0.002044882221487550125, 0.003063384235218505856, 0.004081886248949461587 ),
 .UNSPECIFIED. ) ;
#19927=B_SPLINE_CURVE_WITH_KNOTS ( 'NONE', 3,
 ( #17262, #19823, #4661, #17604, #2113, #32935 ),
 .UNSPECIFIED., .F., .F.,
 ( 4, 2, 4 ),
 ( 0.002044882221487580917, 0.003063384235218526673, 0.004081886248949471996 ),
 .UNSPECIFIED. ) ;
#19963=EDGE_LOOP ( 'NONE', ( #6082, #3752, #27927 ) ) ;
#19969=ORIENTED_EDGE ( 'NONE', *, *, #6818, .T. ) ;
#19976=ORIENTED_EDGE ( 'NONE', *, *, #31797, .F. ) ;
#19983=CARTESIAN_POINT ( 'NONE',  ( 1.750000000000012879, 3.031088913245524097, 1.502314598737187430E-15 ) ) ;
#20020=CARTESIAN_POINT ( 'NONE',  ( 3.500000000000004441, -1.692071238847163928, -2.682267049545481896 ) ) ;
#20049=AXIS2_PLACEMENT_3D ( 'NONE', #14081, #23806, #13412 ) ;
#20073=APPLICATION_CONTEXT ( 'automotive_design' ) ;
#20158=ADVANCED_BREP_SHAPE_REPRESENTATION ( '', ( #12555, #2404 ), #19701 ) ;
#20223=VERTEX_POINT ( 'NONE', #7671 ) ;
#20249=DIRECTION ( 'NONE',  ( -0.000000000000000000, -0.000000000000000000, 1.000000000000000000 ) ) ;
#20320=CONICAL_SURFACE ( 'NONE', #1799, 3.499999999999999556, 1.047197551196589638 ) ;
#20364=EDGE_LOOP ( 'NONE', ( #23895, #19562, #3760, #20482 ) ) ;
#20393=DIRECTION ( 'NONE',  ( 1.000000000000000000, 0.000000000000000000, 0.000000000000000000 ) ) ;
#20476=EDGE_LOOP ( 'NONE', ( #27426, #6302, #5674 ) ) ;
#20481=DIRECTION ( 'NONE',  ( 0.000000000000000000, 0.000000000000000000, -1.000000000000000000 ) ) ;
#20482=ORIENTED_EDGE ( 'NONE', *, *, #22715, .F. ) ;
#20484=AXIS2_PLACEMENT_3D ( 'NONE', #30706, #25751, #15022 ) ;
#20503=CARTESIAN_POINT ( 'NONE',  ( 3.499999999999999556, 0.000000000000000000, 0.000000000000000000 ) ) ;
#20524=EDGE_LOOP ( 'NONE', ( #29104, #8650, #33303, #26590, #18221, #11677 ) ) ;
#20567=ORIENTED_EDGE ( 'NONE', *, *, #13352, .T. ) ;
#20612=VERTEX_POINT ( 'NONE', #19718 ) ;
#20628=B_SPLINE_CURVE_WITH_KNOTS ( 'NONE', 3,
 ( #27741, #14789, #12239, #2022, #12411, #9010 ),
 .UNSPECIFIED., .F., .F.,
 ( 4, 2, 4 ),
 ( 0.002044882221487503288, 0.003063384235218505423, 0.004081886248949507558 ),
 .UNSPECIFIED. ) ;
#20656=VERTEX_POINT ( 'NONE', #11719 ) ;
#20734=FACE_OUTER_BOUND ( 'NONE', #10062, .T. ) ;
#20846=B_SPLINE_CURVE_WITH_KNOTS ( 'NONE', 3,
 ( #24165, #21769, #23995, #31994 ),
 .UNSPECIFIED., .F., .F.,
 ( 4, 4 ),
 ( 2.380739282308437107E-07, 0.002044882221487503288 ),
 .UNSPECIFIED. ) ;
#20859=AXIS2_PLACEMENT_3D ( 'NONE', #25699, #7486, #2201 ) ;
#20915=CARTESIAN_POINT ( 'NONE',  ( 0.000000000000000000, 0.000000000000000000, 3.099999999999998757 ) ) ;
#20919=DIRECTION ( 'NONE',  ( 0.8660254037844359321, -0.5000000000000046629, 0.000000000000000000 ) ) ;
#20924=CARTESIAN_POINT ( 'NONE',  ( -1.650000000000000133, 2.020667218593133001E-16, -2.899999999999999911 ) ) ;
#20978=ORIENTED_EDGE ( 'NONE', *, *, #29706, .F. ) ;
#20982=DIRECTION ( 'NONE',  ( -1.000000000000000000, 0.000000000000000000, 0.000000000000000000 ) ) ;
#21012=CARTESIAN_POINT ( 'NONE',  ( 0.000000000000000000, 0.000000000000000000, -2.899999999999999911 ) ) ;
#21097=DIRECTION ( 'NONE',  ( 1.000000000000000000, 0.000000000000000000, 0.000000000000000000 ) ) ;
#21142=ADVANCED_FACE ( 'NONE', ( #14364 ), #4128, .F. ) ;
#21229=DIRECTION ( 'NONE',  ( -0.000000000000000000, -0.000000000000000000, -1.000000000000000000 ) ) ;
#21237=( NAMED_UNIT ( * ) SI_UNIT ( $, .STERADIAN. ) SOLID_ANGLE_UNIT ( ) );
#21247=CARTESIAN_POINT ( 'NONE',  ( -3.499999999999999112, -1.355464348821715959, -0.1381584212714501159 ) ) ;
#21251=ADVANCED_FACE ( 'NONE', ( #617 ), #25759, .T. ) ;
#21300=DIRECTION ( 'NONE',  ( -1.000000000000000000, 0.000000000000000000, -0.000000000000000000 ) ) ;
#21308=VECTOR ( 'NONE', #16214, 1000.000000000000000 ) ;
#21311=DIRECTION ( 'NONE',  ( 1.000000000000000000, 0.000000000000000000, 0.000000000000000000 ) ) ;
#21335=CARTESIAN_POINT ( 'NONE',  ( -3.499999999999999556, -3.004629197474309385E-15, -2.899999999999999911 ) ) ;
#21402=CARTESIAN_POINT ( 'NONE',  ( -6.830473686658677934E-14, -4.041451884327390331, -2.587392608830344720 ) ) ;
#21439=( GEOMETRIC_REPRESENTATION_CONTEXT ( 3 ) GLOBAL_UNCERTAINTY_ASSIGNED_CONTEXT ( ( #15786 ) ) GLOBAL_UNIT_ASSIGNED_CONTEXT ( ( #15345, #15513, #31355 ) ) REPRESENTATION_CONTEXT ( 'NONE', 'WORKASPACE' ) );
#21509=CARTESIAN_POINT ( 'NONE',  ( 3.499999999999999556, 0.000000000000000000, 0.000000000000000000 ) ) ;
#21522=VERTEX_POINT ( 'NONE', #29707 ) ;
#21568=CIRCLE ( 'NONE', #19189, 2.466666666666999408 ) ;
#21587=CARTESIAN_POINT ( 'NONE',  ( -1.650000000000000133, 2.020667218593133001E-16, -2.629527361626598836 ) ) ;
#21590=VECTOR ( 'NONE', #10568, 1000.000000000000000 ) ;
#21594=EDGE_CURVE ( 'NONE', #7491, #26705, #9704, .T. ) ;
#21646=CARTESIAN_POINT ( 'NONE',  ( 0.000000000000000000, 0.000000000000000000, 0.000000000000000000 ) ) ;
#21698=CARTESIAN_POINT ( 'NONE',  ( 1.525316667890869448E-15, 4.041451884327390331, -2.899999999999999911 ) ) ;
#21724=VERTEX_POINT ( 'NONE', #29888 ) ;
#21769=CARTESIAN_POINT ( 'NONE',  ( 2.927447417349540615, -2.351289329882181534, -2.778243469714872571 ) ) ;
#21787=CARTESIAN_POINT ( 'NONE',  ( -3.500000000000001332, 2.020725942163676070, -2.899999999999999911 ) ) ;
#21796=ORIENTED_EDGE ( 'NONE', *, *, #9759, .F. ) ;
#21806=CARTESIAN_POINT ( 'NONE',  ( 1.750000000000014211, 3.031088913245526317, -2.899999999999999911 ) ) ;
#21837=CARTESIAN_POINT ( 'NONE',  ( 2.343682934607771440, 2.688325911136448809, -2.870065989602863965 ) ) ;
#21852=CARTESIAN_POINT ( 'NONE',  ( 0.000000000000000000, 0.000000000000000000, -2.899999999999999911 ) ) ;
#21897=AXIS2_PLACEMENT_3D ( 'NONE', #26493, #605, #13551 ) ;
#21909=CARTESIAN_POINT ( 'NONE',  ( -3.499999999999999556, -3.004629197474309385E-15, -2.899999999999999911 ) ) ;
#21912=CARTESIAN_POINT ( 'NONE',  ( -2.000000000000000000, 0.000000000000000000, -2.874600000000001376 ) ) ;
#21999=ADVANCED_FACE ( 'NONE', ( #2622 ), #4488, .F. ) ;
#22022=PRODUCT_DEFINITION_CONTEXT ( 'detailed design', #11815, 'design' ) ;
#22058=ADVANCED_FACE ( 'NONE', ( #6928 ), #14596, .F. ) ;
#22071=DIRECTION ( 'NONE',  ( -0.000000000000000000, -0.000000000000000000, 1.000000000000000000 ) ) ;
#22080=CARTESIAN_POINT ( 'NONE',  ( 0.000000000000000000, 0.000000000000000000, -2.874600000000001376 ) ) ;
#22102=CIRCLE ( 'NONE', #20484, 1.033333333332998372 ) ;
#22112=FACE_OUTER_BOUND ( 'NONE', #19963, .T. ) ;
#22145=AXIS2_PLACEMENT_3D ( 'NONE', #2056, #1544, #32709 ) ;
#22152=DIRECTION ( 'NONE',  ( -0.000000000000000000, -0.000000000000000000, 1.000000000000000000 ) ) ;
#22226=CARTESIAN_POINT ( 'NONE',  ( -1.452965002680439266, 3.202582148906723436, -2.900000000000002132 ) ) ;
#22302=DIRECTION ( 'NONE',  ( -0.000000000000000000, -0.000000000000000000, 1.000000000000000000 ) ) ;
#22313=VERTEX_POINT ( 'NONE', #26617 ) ;
#22334=CARTESIAN_POINT ( 'NONE',  ( 2.927447417349540615, -2.351289329882181534, -0.1217565302851272152 ) ) ;
#22353=AXIS2_PLACEMENT_3D ( 'NONE', #5241, #17686, #20919 ) ;
#22410=EDGE_CURVE ( 'NONE', #5483, #258, #6959, .T. ) ;
#22427=EDGE_CURVE ( 'NONE', #15312, #32873, #32435, .T. ) ;
#22437=ORIENTED_EDGE ( 'NONE', *, *, #18761, .T. ) ;
#22479=AXIS2_PLACEMENT_3D ( 'NONE', #27518, #22071, #27689 ) ;
#22527=ORIENTED_EDGE ( 'NONE', *, *, #8750, .F. ) ;
#22585=DIRECTION ( 'NONE',  ( -0.000000000000000000, -0.000000000000000000, 1.000000000000000000 ) ) ;
#22656=DIRECTION ( 'NONE',  ( 1.000000000000000000, 0.000000000000000000, 0.000000000000000000 ) ) ;
#22694=ORIENTED_EDGE ( 'NONE', *, *, #27047, .F. ) ;
#22715=EDGE_CURVE ( 'NONE', #1780, #16312, #22102, .T. ) ;
#22774=CARTESIAN_POINT ( 'NONE',  ( 0.000000000000000000, 0.000000000000000000, -25.03750572909317285 ) ) ;
#22795=DIRECTION ( 'NONE',  ( -0.000000000000000000, -0.000000000000000000, 1.000000000000000000 ) ) ;
#22825=ORIENTED_EDGE ( 'NONE', *, *, #12519, .T. ) ;
#23032=EDGE_LOOP ( 'NONE', ( #25329, #20567, #8011, #11177, #19417, #12170 ) ) ;
#23047=COLOUR_RGB ( '', 0.40784314, 0.44705882, 0.49803922) ;
#23057=CARTESIAN_POINT ( 'NONE',  ( 1.750000000000014211, 3.031088913245526317, -2.899999999999999911 ) ) ;
#23084=ORIENTED_EDGE ( 'NONE', *, *, #17645, .F. ) ;
#23125=CARTESIAN_POINT ( 'NONE',  ( 0.000000000000000000, 0.000000000000000000, 0.000000000000000000 ) ) ;
#23151=DIRECTION ( 'NONE',  ( -1.000000000000000000, 0.000000000000000000, 0.000000000000000000 ) ) ;
#23169=B_SPLINE_CURVE_WITH_KNOTS ( 'NONE', 3,
 ( #19090, #3759, #11429, #21806 ),
 .UNSPECIFIED., .F., .F.,
 ( 4, 4 ),
 ( 2.380739282171097332E-07, 0.002044882221487550125 ),
 .UNSPECIFIED. ) ;
#23225=CARTESIAN_POINT ( 'NONE',  ( 3.500000000000004441, 0.3416723310689536164, -2.988332237913170807E-15 ) ) ;
#23246=CARTESIAN_POINT ( 'NONE',  ( 1.517883041479706208E-15, 4.041451884327390331, -0.3126073911696551910 ) ) ;
#23304=AXIS2_PLACEMENT_3D ( 'NONE', #23915, #3135, #579 ) ;
#23343=CARTESIAN_POINT ( 'NONE',  ( 2.000000000000000000, 2.449293598294706414E-16, -2.874600000000001376 ) ) ;
#23401=CARTESIAN_POINT ( 'NONE',  ( 3.500000000000004885, 2.020725942163702715, -0.3126073911696551910 ) ) ;
#23433=DIRECTION ( 'NONE',  ( -0.000000000000000000, -0.000000000000000000, 1.000000000000000000 ) ) ;
#23454=FACE_OUTER_BOUND ( 'NONE', #24546, .T. ) ;
#23468=DIRECTION ( 'NONE',  ( 1.000000000000000000, 0.000000000000000000, 0.000000000000000000 ) ) ;
#23526=DIRECTION ( 'NONE',  ( 1.000000000000000000, 0.000000000000000000, 0.000000000000000000 ) ) ;
#23532=EDGE_CURVE ( 'NONE', #7491, #15536, #397, .T. ) ;
#23541=FACE_OUTER_BOUND ( 'NONE', #30824, .T. ) ;
#23586=VERTEX_POINT ( 'NONE', #21587 ) ;
#23660=ORIENTED_EDGE ( 'NONE', *, *, #33526, .T. ) ;
#23665=LINE ( 'NONE', #23343, #21590 ) ;
#23693=VERTEX_POINT ( 'NONE', #11046 ) ;
#23702=CARTESIAN_POINT ( 'NONE',  ( -6.830473686658677934E-14, -4.041451884327390331, -0.3126073911696551910 ) ) ;
#23782=DIRECTION ( 'NONE',  ( -0.000000000000000000, -0.000000000000000000, 1.000000000000000000 ) ) ;
#23806=DIRECTION ( 'NONE',  ( -0.000000000000000000, -0.000000000000000000, 1.000000000000000000 ) ) ;
#23828=EDGE_CURVE ( 'NONE', #11491, #14565, #31432, .T. ) ;
#23866=CARTESIAN_POINT ( 'NONE',  ( 0.000000000000000000, 0.000000000000000000, 0.000000000000000000 ) ) ;
#23895=ORIENTED_EDGE ( 'NONE', *, *, #33053, .T. ) ;
#23915=CARTESIAN_POINT ( 'NONE',  ( 0.000000000000000000, 0.000000000000000000, -2.899999999999999911 ) ) ;
#23927=EDGE_CURVE ( 'NONE', #2969, #10366, #12213, .T. ) ;
#23939=ORIENTED_EDGE ( 'NONE', *, *, #6818, .F. ) ;
#23995=CARTESIAN_POINT ( 'NONE',  ( 2.346298152288388117, -2.686816014504594730, -2.899999999999981704 ) ) ;
#24018=EDGE_CURVE ( 'NONE', #20656, #24119, #19922, .T. ) ;
#24067=PLANE ( 'NONE',  #12693 ) ;
#24072=ADVANCED_FACE ( 'NONE', ( #13385 ), #14540, .T. ) ;
#24082=CARTESIAN_POINT ( 'NONE',  ( -3.499999999999997780, -2.020725942163714262, -0.3126073911696551910 ) ) ;
#24098=ADVANCED_FACE ( 'NONE', ( #23454 ), #4767, .T. ) ;
#24099=DIRECTION ( 'NONE',  ( 1.000000000000000000, 0.000000000000000000, 0.000000000000000000 ) ) ;
#24119=VERTEX_POINT ( 'NONE', #5395 ) ;
#24126=CONICAL_SURFACE ( 'NONE', #17053, 3.499999999999999556, 1.047197551196589638 ) ;
#24130=EDGE_CURVE ( 'NONE', #23693, #20612, #31620, .T. ) ;
#24165=CARTESIAN_POINT ( 'NONE',  ( 3.499999999999993339, -2.020725942163723143, -2.587392608830344720 ) ) ;
#24192=ORIENTED_EDGE ( 'NONE', *, *, #21594, .T. ) ;
#24201=DIRECTION ( 'NONE',  ( -0.000000000000000000, -0.000000000000000000, 1.000000000000000000 ) ) ;
#24211=CARTESIAN_POINT ( 'NONE',  ( -1.750000000000016209, -3.031088913245524985, -2.899999999999999911 ) ) ;
#24278=B_SPLINE_CURVE_WITH_KNOTS ( 'NONE', 3,
 ( #6358, #32754, #1750, #19983 ),
 .UNSPECIFIED., .F., .F.,
 ( 4, 4 ),
 ( 2.380739282168500117E-07, 0.002044882221487550125 ),
 .UNSPECIFIED. ) ;
#24286=SURFACE_STYLE_USAGE ( .BOTH. , #19020 ) ;
#24296=CARTESIAN_POINT ( 'NONE',  ( -3.499999999999996891, -1.692071238847157710, -0.2177329504545129080 ) ) ;
#24318=EDGE_LOOP ( 'NONE', ( #13137, #33640, #32364, #404, #8856, #15057 ) ) ;
#24361=FACE_BOUND ( 'NONE', #12819, .T. ) ;
#24375=DIRECTION ( 'NONE',  ( 0.000000000000000000, 0.000000000000000000, 1.000000000000000000 ) ) ;
#24405=CARTESIAN_POINT ( 'NONE',  ( -3.499999999999999112, -1.355464348821716625, -2.761841578728549962 ) ) ;
#24442=EDGE_LOOP ( 'NONE', ( #31658, #3994, #22527, #20978 ) ) ;
#24454=EDGE_LOOP ( 'NONE', ( #4263, #31538, #13356 ) ) ;
#24538=LINE ( 'NONE', #6300, #33624 ) ;
#24546=EDGE_LOOP ( 'NONE', ( #22694, #29227, #2216, #19976 ) ) ;
#24556=EDGE_CURVE ( 'NONE', #13276, #16396, #10600, .T. ) ;
#24577=CARTESIAN_POINT ( 'NONE',  ( 0.000000000000000000, 0.000000000000000000, 9.480888224575629408 ) ) ;
#24630=DIRECTION ( 'NONE',  ( 1.000000000000000000, 0.000000000000000000, 0.000000000000000000 ) ) ;
#24632=CIRCLE ( 'NONE', #21897, 1.649999999999999911 ) ;
#24728=B_SPLINE_CURVE_WITH_KNOTS ( 'NONE', 3,
 ( #17730, #17557, #27949, #11947 ),
 .UNSPECIFIED., .F., .F.,
 ( 4, 4 ),
 ( 2.380739282167303683E-07, 0.002044882221487520201 ),
 .UNSPECIFIED. ) ;
#24757=EDGE_CURVE ( 'NONE', #20656, #15312, #17827, .T. ) ;
#24825=ORIENTED_EDGE ( 'NONE', *, *, #115, .F. ) ;
#24869=EDGE_CURVE ( 'NONE', #8405, #14565, #24538, .T. ) ;
#24903=ORIENTED_EDGE ( 'NONE', *, *, #13066, .T. ) ;
#24921=DIRECTION ( 'NONE',  ( 1.000000000000000000, 0.000000000000000000, 0.000000000000000000 ) ) ;
#24960=CIRCLE ( 'NONE', #3186, 3.499999999999999556 ) ;
#24988=ADVANCED_FACE ( 'NONE', ( #14309 ), #25467, .T. ) ;
#25065=DIRECTION ( 'NONE',  ( 0.000000000000000000, 0.000000000000000000, 1.000000000000000000 ) ) ;
#25152=CARTESIAN_POINT ( 'NONE',  ( 2.000000000000000888, 0.000000000000000000, -25.03750572909317285 ) ) ;
#25217=ORIENTED_EDGE ( 'NONE', *, *, #24869, .T. ) ;
#25234=CARTESIAN_POINT ( 'NONE',  ( 3.500000000000004885, -2.020725942163716038, -2.899999999999999911 ) ) ;
#25272=DIRECTION ( 'NONE',  ( 1.000000000000000000, 0.000000000000000000, 0.000000000000000000 ) ) ;
#25329=ORIENTED_EDGE ( 'NONE', *, *, #3314, .T. ) ;
#25344=CARTESIAN_POINT ( 'NONE',  ( 2.000000000000000888, 0.000000000000000000, -2.899999999999999911 ) ) ;
#25359=CARTESIAN_POINT ( 'NONE',  ( -3.499999999999999556, -3.004629197474309385E-15, 0.000000000000000000 ) ) ;
#25467=CONICAL_SURFACE ( 'NONE', #10793, 3.499999999999999556, 1.047197551196589638 ) ;
#25616=ORIENTED_EDGE ( 'NONE', *, *, #23828, .T. ) ;
#25637=EDGE_CURVE ( 'NONE', #32991, #13221, #9360, .T. ) ;
#25672=ORIENTED_EDGE ( 'NONE', *, *, #26191, .T. ) ;
#25692=LINE ( 'NONE', #20924, #11892 ) ;
#25699=CARTESIAN_POINT ( 'NONE',  ( 3.469446951953614189E-15, -4.041451884327432076, -2.899999999999999911 ) ) ;
#25715=CARTESIAN_POINT ( 'NONE',  ( -3.499999999999997780, -2.020725942163716038, -2.899999999999999911 ) ) ;
#25748=CARTESIAN_POINT ( 'NONE',  ( -1.750000000000016209, -3.031088913245524985, 0.000000000000000000 ) ) ;
#25751=DIRECTION ( 'NONE',  ( 0.000000000000000000, -1.000000000000000000, 0.000000000000000000 ) ) ;
#25759=CONICAL_SURFACE ( 'NONE', #1265, 3.499999999999999556, 1.047197551196589638 ) ;
#25786=CARTESIAN_POINT ( 'NONE',  ( 3.500000000000004885, 0.6879904500768362352, -0.03016324292412390917 ) ) ;
#25808=ORIENTED_EDGE ( 'NONE', *, *, #24018, .T. ) ;
#25813=B_SPLINE_CURVE_WITH_KNOTS ( 'NONE', 3,
 ( #26451, #26779, #24405, #16387, #8403, #21335 ),
 .UNSPECIFIED., .F., .F.,
 ( 4, 2, 4 ),
 ( 0.003605240635278501252, 0.004627368318297491422, 0.005649496001316482025 ),
 .UNSPECIFIED. ) ;
#25844=ORIENTED_EDGE ( 'NONE', *, *, #19789, .F. ) ;
#25918=ADVANCED_FACE ( 'NONE', ( #20734 ), #1533, .T. ) ;
#25992=CARTESIAN_POINT ( 'NONE',  ( -1.750000000000014211, 3.031088913245526317, 0.000000000000000000 ) ) ;
#26060=AXIS2_PLACEMENT_3D ( 'NONE', #27109, #16366, #3927 ) ;
#26078=SHAPE_DEFINITION_REPRESENTATION ( #9999, #30243 ) ;
#26088=CARTESIAN_POINT ( 'NONE',  ( 0.000000000000000000, 0.000000000000000000, 3.100000000000000533 ) ) ;
#26191=EDGE_CURVE ( 'NONE', #15536, #9440, #24960, .T. ) ;
#26397=ADVANCED_FACE ( 'NONE', ( #11515 ), #19177, .F. ) ;
#26419=ORIENTED_EDGE ( 'NONE', *, *, #16463, .T. ) ;
#26450=B_SPLINE_CURVE_WITH_KNOTS ( 'NONE', 3,
 ( #17562, #22334, #11952, #7009 ),
 .UNSPECIFIED., .F., .F.,
 ( 4, 4 ),
 ( 2.380739282308591161E-07, 0.002044882221487502854 ),
 .UNSPECIFIED. ) ;
#26451=CARTESIAN_POINT ( 'NONE',  ( -3.499999999999997780, -2.020725942163714262, -2.587392608830344720 ) ) ;
#26493=CARTESIAN_POINT ( 'NONE',  ( 0.000000000000000000, 0.000000000000000000, 2.066666666667000385 ) ) ;
#26523=CONICAL_SURFACE ( 'NONE', #2620, 3.499999999999999556, 1.047197551196589638 ) ;
#26559=DIRECTION ( 'NONE',  ( -1.000000000000000000, -8.584654849926598947E-16, 0.000000000000000000 ) ) ;
#26577=ORIENTED_EDGE ( 'NONE', *, *, #4594, .T. ) ;
#26590=ORIENTED_EDGE ( 'NONE', *, *, #1334, .F. ) ;
#26592=CARTESIAN_POINT ( 'NONE',  ( -2.428571428571428381, 2.974142226500714333E-16, 3.100000000000000533 ) ) ;
#26617=CARTESIAN_POINT ( 'NONE',  ( 1.649999999999999911, 0.000000000000000000, 2.066666666667000385 ) ) ;
#26705=VERTEX_POINT ( 'NONE', #12188 ) ;
#26756=ORIENTED_EDGE ( 'NONE', *, *, #8750, .T. ) ;
#26779=CARTESIAN_POINT ( 'NONE',  ( -3.499999999999996891, -1.692071238847158821, -2.682267049545485893 ) ) ;
#26780=DIRECTION ( 'NONE',  ( 0.000000000000000000, 0.000000000000000000, 1.000000000000000000 ) ) ;
#26963=ORIENTED_EDGE ( 'NONE', *, *, #26191, .F. ) ;
#27009=CARTESIAN_POINT ( 'NONE',  ( 0.000000000000000000, 0.000000000000000000, -2.899999999999999911 ) ) ;
#27047=EDGE_CURVE ( 'NONE', #4795, #19546, #382, .T. ) ;
#27048=CIRCLE ( 'NONE', #31420, 1.650000000000000133 ) ;
#27087=ADVANCED_FACE ( 'NONE', ( #32673 ), #19416, .T. ) ;
#27109=CARTESIAN_POINT ( 'NONE',  ( 0.000000000000000000, 0.000000000000000000, 3.099999999999998757 ) ) ;
#27186=CIRCLE ( 'NONE', #2174, 2.000000000000000000 ) ;
#27251=EDGE_CURVE ( 'NONE', #7491, #4173, #15084, .T. ) ;
#27258=DIRECTION ( 'NONE',  ( -0.000000000000000000, -0.000000000000000000, 1.000000000000000000 ) ) ;
#27322=ORIENTED_EDGE ( 'NONE', *, *, #723, .T. ) ;
#27337=ORIENTED_EDGE ( 'NONE', *, *, #10969, .F. ) ;
#27426=ORIENTED_EDGE ( 'NONE', *, *, #115, .T. ) ;
#27487=CARTESIAN_POINT ( 'NONE',  ( -6.999999999999969802, -1.734723475976807094E-14, -2.899999999999999911 ) ) ;
#27518=CARTESIAN_POINT ( 'NONE',  ( 0.000000000000000000, 0.000000000000000000, 2.066666666666666430 ) ) ;
#27544=ORIENTED_EDGE ( 'NONE', *, *, #17100, .T. ) ;
#27571=CIRCLE ( 'NONE', #6913, 3.500000000000000444 ) ;
#27589=CIRCLE ( 'NONE', #6363, 3.500000000000000444 ) ;
#27648=CARTESIAN_POINT ( 'NONE',  ( -3.499999999999999112, 0.6879904500768249109, -0.03016324292412032870 ) ) ;
#27671=AXIS2_PLACEMENT_3D ( 'NONE', #22080, #12025, #4185 ) ;
#27689=DIRECTION ( 'NONE',  ( 1.000000000000000000, 0.000000000000000000, 0.000000000000000000 ) ) ;
#27731=CARTESIAN_POINT ( 'NONE',  ( 0.000000000000000000, 0.000000000000000000, 0.000000000000000000 ) ) ;
#27737=CARTESIAN_POINT ( 'NONE',  ( -2.466666666666999408, 3.020795437897212205E-16, 2.066666666667000385 ) ) ;
#27741=CARTESIAN_POINT ( 'NONE',  ( 1.750000000000016209, -3.031088913245524985, -2.899999999999999911 ) ) ;
#27801=ORIENTED_EDGE ( 'NONE', *, *, #4311, .T. ) ;
#27829=ADVANCED_FACE ( 'NONE', ( #14706 ), #7053, .F. ) ;
#27908=FACE_OUTER_BOUND ( 'NONE', #32789, .T. ) ;
#27927=ORIENTED_EDGE ( 'NONE', *, *, #3864, .F. ) ;
#27929=EDGE_CURVE ( 'NONE', #258, #24119, #6820, .T. ) ;
#27949=CARTESIAN_POINT ( 'NONE',  ( -2.346298152288380567, 2.686816014504556538, 2.727401335159862919E-15 ) ) ;
#28017=CARTESIAN_POINT ( 'NONE',  ( -1.750000000000016209, -3.031088913245524985, 0.000000000000000000 ) ) ;
#28058=EDGE_CURVE ( 'NONE', #21522, #23586, #27048, .T. ) ;
#28078=CARTESIAN_POINT ( 'NONE',  ( 1.750000000000016209, -3.031088913245524985, 0.000000000000000000 ) ) ;
#28085=PLANE ( 'NONE',  #20859 ) ;
#28196=CIRCLE ( 'NONE', #23304, 3.499999999999999556 ) ;
#28217=CIRCLE ( 'NONE', #18422, 2.000000000000000000 ) ;
#28240=DIRECTION ( 'NONE',  ( -1.000000000000000000, 0.000000000000000000, 0.000000000000000000 ) ) ;
#28419=EDGE_CURVE ( 'NONE', #697, #5483, #17564, .T. ) ;
#28425=DIRECTION ( 'NONE',  ( 0.000000000000000000, 0.000000000000000000, 1.000000000000000000 ) ) ;
#28432=DIRECTION ( 'NONE',  ( -0.000000000000000000, -0.000000000000000000, 1.000000000000000000 ) ) ;
#28442=ORIENTED_EDGE ( 'NONE', *, *, #22427, .F. ) ;
#28468=SURFACE_STYLE_USAGE ( .BOTH. , #22 ) ;
#28490=EDGE_CURVE ( 'NONE', #32873, #4795, #4105, .T. ) ;
#28491=ORIENTED_EDGE ( 'NONE', *, *, #27251, .F. ) ;
#28587=DIRECTION ( 'NONE',  ( 1.000000000000000000, 0.000000000000000000, 0.000000000000000000 ) ) ;
#28713=EDGE_CURVE ( 'NONE', #32991, #17505, #16171, .T. ) ;
#28736=CARTESIAN_POINT ( 'NONE',  ( 0.000000000000000000, 0.000000000000000000, 2.066666666667000385 ) ) ;
#28801=FILL_AREA_STYLE_COLOUR ( '', #30700 ) ;
#28841=CARTESIAN_POINT ( 'NONE',  ( 3.500000000000004885, 1.693985822988438139, -0.2182856432892083254 ) ) ;
#28863=ORIENTED_EDGE ( 'NONE', *, *, #11801, .T. ) ;
#28896=DIRECTION ( 'NONE',  ( -1.000000000000000000, 0.000000000000000000, 0.000000000000000000 ) ) ;
#28912=DIRECTION ( 'NONE',  ( 1.000000000000000000, 0.000000000000000000, 0.000000000000000000 ) ) ;
#28933=EDGE_LOOP ( 'NONE', ( #27337, #28442, #17191 ) ) ;
#29035=CONICAL_SURFACE ( 'NONE', #18704, 3.499999999999999556, 1.047197551196589638 ) ;
#29088=CARTESIAN_POINT ( 'NONE',  ( -3.499999999999999556, -3.004629197474309385E-15, 0.000000000000000000 ) ) ;
#29104=ORIENTED_EDGE ( 'NONE', *, *, #22427, .T. ) ;
#29180=CARTESIAN_POINT ( 'NONE',  ( 3.500000000000004441, -1.692071238847164372, -0.2177329504545181260 ) ) ;
#29191=CARTESIAN_POINT ( 'NONE',  ( -1.452965002680439710, 3.202582148906722992, 2.797749824780954020E-15 ) ) ;
#29200=FACE_OUTER_BOUND ( 'NONE', #3943, .T. ) ;
#29227=ORIENTED_EDGE ( 'NONE', *, *, #8681, .T. ) ;
#29276=AXIS2_PLACEMENT_3D ( 'NONE', #5686, #10486, #18974 ) ;
#29408=( NAMED_UNIT ( * ) SI_UNIT ( $, .STERADIAN. ) SOLID_ANGLE_UNIT ( ) );
#29482=ADVANCED_FACE ( 'NONE', ( #31804 ), #8102, .T. ) ;
#29553=ORIENTED_EDGE ( 'NONE', *, *, #6380, .T. ) ;
#29667=CARTESIAN_POINT ( 'NONE',  ( 2.428571428571428381, 0.000000000000000000, 3.100000000000000533 ) ) ;
#29706=EDGE_CURVE ( 'NONE', #23586, #21724, #17478, .T. ) ;
#29707=CARTESIAN_POINT ( 'NONE',  ( 1.650000000000000133, 0.000000000000000000, -2.629527361626598836 ) ) ;
#29737=DIRECTION ( 'NONE',  ( 0.000000000000000000, 0.000000000000000000, 1.000000000000000000 ) ) ;
#29770=ORIENTED_EDGE ( 'NONE', *, *, #1423, .T. ) ;
#29790=AXIS2_PLACEMENT_3D ( 'NONE', #2011, #22795, #132 ) ;
#29794=DIRECTION ( 'NONE',  ( 1.224646799147353207E-16, 1.000000000000000000, 0.000000000000000000 ) ) ;
#29824=CARTESIAN_POINT ( 'NONE',  ( 0.000000000000000000, 0.000000000000000000, 0.000000000000000000 ) ) ;
#29827=VERTEX_POINT ( 'NONE', #7437 ) ;
#29869=DIRECTION ( 'NONE',  ( -0.000000000000000000, -0.000000000000000000, 1.000000000000000000 ) ) ;
#29888=CARTESIAN_POINT ( 'NONE',  ( -2.000000000000000000, 0.000000000000000000, -2.874600000000001376 ) ) ;
#29930=DIRECTION ( 'NONE',  ( -0.8191520442889872466, 0.000000000000000000, -0.5735764363510525987 ) ) ;
#29974=CARTESIAN_POINT ( 'NONE',  ( -3.499999999999997780, -2.020725942163714262, -2.587392608830344720 ) ) ;
#29979=ORIENTED_EDGE ( 'NONE', *, *, #24757, .F. ) ;
#30020=CARTESIAN_POINT ( 'NONE',  ( 2.466666666666999408, 0.000000000000000000, 3.099999999999998757 ) ) ;
#30062=LINE ( 'NONE', #1953, #15372 ) ;
#30119=EDGE_LOOP ( 'NONE', ( #7793, #8110, #4552 ) ) ;
#30143=CARTESIAN_POINT ( 'NONE',  ( -2.047034997319599814, -2.859595677584359841, -2.899999999999983036 ) ) ;
#30235=CARTESIAN_POINT ( 'NONE',  ( -3.500000000000001332, 2.020725942163676070, -0.3126073911696459207 ) ) ;
#30237=CARTESIAN_POINT ( 'NONE',  ( -0.2855619784720673793, 3.876582599186217948, -2.682579934988236658 ) ) ;
#30243=SHAPE_REPRESENTATION ( 'torque nut 01_iso_ISO 7040-M4-N', ( #2404 ), #19701 ) ;
#30285=ORIENTED_EDGE ( 'NONE', *, *, #32029, .T. ) ;
#30294=DIRECTION ( 'NONE',  ( -1.000000000000000000, 1.224646799147352714E-16, 0.000000000000000000 ) ) ;
#30430=CONICAL_SURFACE ( 'NONE', #15737, 3.499999999999999556, 1.047197551196589638 ) ;
#30454=AXIS2_PLACEMENT_3D ( 'NONE', #9018, #22302, #14129 ) ;
#30592=CARTESIAN_POINT ( 'NONE',  ( 3.499999999999996891, 0.000000000000000000, 2.066666666666666430 ) ) ;
#30700=COLOUR_RGB ( '', 0.40784314, 0.44705882, 0.49803922) ;
#30706=CARTESIAN_POINT ( 'NONE',  ( 2.466666666666999408, 0.000000000000000000, 2.066666666667000385 ) ) ;
#30707=B_SPLINE_CURVE_WITH_KNOTS ( 'NONE', 3,
 ( #3115, #13665, #21837, #5505, #15894, #5831 ),
 .UNSPECIFIED., .F., .F.,
 ( 4, 2, 4 ),
 ( 0.002044882221487550125, 0.003063384235218505856, 0.004081886248949461587 ),
 .UNSPECIFIED. ) ;
#30814=CARTESIAN_POINT ( 'NONE',  ( 1.156317065392248100, -3.373851915354654896, -0.02993401039715992348 ) ) ;
#30824=EDGE_LOOP ( 'NONE', ( #12844, #5097, #7376 ) ) ;
#30827=EDGE_CURVE ( 'NONE', #20612, #20656, #24278, .T. ) ;
#30867=B_SPLINE_CURVE_WITH_KNOTS ( 'NONE', 3,
 ( #5514, #29191, #2471, #13516, #81, #23246 ),
 .UNSPECIFIED., .F., .F.,
 ( 4, 2, 4 ),
 ( 0.002044882221487520201, 0.003063384235218495882, 0.004081886248949471996 ),
 .UNSPECIFIED. ) ;
#30885=CARTESIAN_POINT ( 'NONE',  ( -2.466666666666999408, 3.653529617456472921E-16, 3.099999999999998757 ) ) ;
#30905=CARTESIAN_POINT ( 'NONE',  ( 3.500000000000004441, 1.362959798491822250, -0.1397344949837900085 ) ) ;
#31023=DIRECTION ( 'NONE',  ( 1.000000000000000000, 0.000000000000000000, 0.000000000000000000 ) ) ;
#31042=ORIENTED_EDGE ( 'NONE', *, *, #6007, .T. ) ;
#31086=AXIS2_PLACEMENT_3D ( 'NONE', #31478, #6361, #28912 ) ;
#31103=AXIS2_PLACEMENT_3D ( 'NONE', #27487, #17433, #4142 ) ;
#31188=B_SPLINE_CURVE_WITH_KNOTS ( 'NONE', 3,
 ( #16127, #24296, #21247, #964, #11364, #29088 ),
 .UNSPECIFIED., .F., .F.,
 ( 4, 2, 4 ),
 ( 0.003605240635278502120, 0.004627368318297491422, 0.005649496001316481157 ),
 .UNSPECIFIED. ) ;
#31248=FACE_OUTER_BOUND ( 'NONE', #3439, .T. ) ;
#31300=ORIENTED_EDGE ( 'NONE', *, *, #5768, .T. ) ;
#31302=CARTESIAN_POINT ( 'NONE',  ( 0.000000000000000000, 0.000000000000000000, -2.899999999999999911 ) ) ;
#31355=( NAMED_UNIT ( * ) SI_UNIT ( $, .STERADIAN. ) SOLID_ANGLE_UNIT ( ) );
#31420=AXIS2_PLACEMENT_3D ( 'NONE', #18947, #13832, #8885 ) ;
#31432=CIRCLE ( 'NONE', #16728, 2.428571428571428381 ) ;
#31478=CARTESIAN_POINT ( 'NONE',  ( 0.000000000000000000, 0.000000000000000000, 0.000000000000000000 ) ) ;
#31502=ORIENTED_EDGE ( 'NONE', *, *, #30827, .F. ) ;
#31538=ORIENTED_EDGE ( 'NONE', *, *, #9176, .F. ) ;
#31576=DIRECTION ( 'NONE',  ( 1.000000000000000000, 0.000000000000000000, 0.000000000000000000 ) ) ;
#31597=EDGE_CURVE ( 'NONE', #16396, #20223, #11253, .T. ) ;
#31620=LINE ( 'NONE', #16105, #2599 ) ;
#31658=ORIENTED_EDGE ( 'NONE', *, *, #19742, .T. ) ;
#31694=PLANE ( 'NONE',  #17072 ) ;
#31701=DIRECTION ( 'NONE',  ( 1.000000000000000000, 0.000000000000000000, 0.000000000000000000 ) ) ;
#31755=CIRCLE ( 'NONE', #15977, 1.649999999999999911 ) ;
#31759=CARTESIAN_POINT ( 'NONE',  ( 0.000000000000000000, 0.000000000000000000, -2.899999999999999911 ) ) ;
#31797=EDGE_CURVE ( 'NONE', #19546, #16312, #21568, .T. ) ;
#31804=FACE_OUTER_BOUND ( 'NONE', #1913, .T. ) ;
#31841=CARTESIAN_POINT ( 'NONE',  ( -3.500000000000001332, 2.020725942163676070, -2.899999999999999911 ) ) ;
#31856=DIRECTION ( 'NONE',  ( 0.000000000000000000, 0.000000000000000000, -1.000000000000000000 ) ) ;
#31943=CARTESIAN_POINT ( 'NONE',  ( 2.343682934607771440, 2.688325911136448809, -0.02993401039713653594 ) ) ;
#31994=CARTESIAN_POINT ( 'NONE',  ( 1.750000000000016209, -3.031088913245524985, -2.899999999999999911 ) ) ;
#32029=EDGE_CURVE ( 'NONE', #14565, #11491, #13765, .T. ) ;
#32123=DIRECTION ( 'NONE',  ( -0.000000000000000000, -0.000000000000000000, 1.000000000000000000 ) ) ;
#32176=PLANE ( 'NONE',  #18531 ) ;
#32202=CARTESIAN_POINT ( 'NONE',  ( 3.499999999999999556, 0.000000000000000000, 0.000000000000000000 ) ) ;
#32285=ORIENTED_EDGE ( 'NONE', *, *, #17294, .F. ) ;
#32326=CARTESIAN_POINT ( 'NONE',  ( -3.500000000000001332, 2.020725942163708488, -2.587392608830344720 ) ) ;
#32364=ORIENTED_EDGE ( 'NONE', *, *, #3864, .T. ) ;
#32435=CIRCLE ( 'NONE', #6886, 3.500000000000000444 ) ;
#32459=SHAPE_REPRESENTATION_RELATIONSHIP ( 'NONE' , 'NONE' ,  #30243, #20158 ) ;
#32498=DIRECTION ( 'NONE',  ( 0.000000000000000000, 0.000000000000000000, -1.000000000000000000 ) ) ;
#32501=FACE_OUTER_BOUND ( 'NONE', #2958, .T. ) ;
#32526=ORIENTED_EDGE ( 'NONE', *, *, #25637, .T. ) ;
#32552=CARTESIAN_POINT ( 'NONE',  ( -3.499999999999996891, 4.286263797015732651E-16, 2.066666666666666430 ) ) ;
#32652=ORIENTED_EDGE ( 'NONE', *, *, #5768, .F. ) ;
#32673=FACE_OUTER_BOUND ( 'NONE', #20364, .T. ) ;
#32698=ADVANCED_FACE ( 'NONE', ( #10050 ), #24126, .T. ) ;
#32709=DIRECTION ( 'NONE',  ( 1.000000000000000000, 0.000000000000000000, 0.000000000000000000 ) ) ;
#32754=CARTESIAN_POINT ( 'NONE',  ( 0.5725525826504701543, 3.710888496608923059, -0.1217565302851157799 ) ) ;
#32762=CARTESIAN_POINT ( 'NONE',  ( 3.500000000000004885, 1.693985822988437917, -2.681714356710791058 ) ) ;
#32789=EDGE_LOOP ( 'NONE', ( #3880, #18837, #15151, #23939 ) ) ;
#32834=MECHANICAL_DESIGN_GEOMETRIC_PRESENTATION_REPRESENTATION('',(#7268),#6181);
#32866=ADVANCED_FACE ( 'NONE', ( #33203 ), #28085, .T. ) ;
#32873=VERTEX_POINT ( 'NONE', #25359 ) ;
#32900=EDGE_CURVE ( 'NONE', #8405, #29827, #3430, .T. ) ;
#32908=ADVANCED_FACE ( 'NONE', ( #15644 ), #20320, .T. ) ;
#32931=CARTESIAN_POINT ( 'NONE',  ( -3.500000000000000888, 1.362959798491803154, -0.1397344949837840966 ) ) ;
#32935=CARTESIAN_POINT ( 'NONE',  ( -3.499999999999997780, -2.020725942163714262, -0.3126073911696551910 ) ) ;
#32960=CARTESIAN_POINT ( 'NONE',  ( 3.499999999999993339, -2.020725942163723143, -2.587392608830344720 ) ) ;
#32971=DIRECTION ( 'NONE',  ( 1.000000000000000000, 0.000000000000000000, 0.000000000000000000 ) ) ;
#32991=VERTEX_POINT ( 'NONE', #12583 ) ;
#33040=ORIENTED_EDGE ( 'NONE', *, *, #15990, .T. ) ;
#33053=EDGE_CURVE ( 'NONE', #1780, #4795, #11085, .T. ) ;
#33063=DIRECTION ( 'NONE',  ( -0.000000000000000000, -0.000000000000000000, 1.000000000000000000 ) ) ;
#33139=PRODUCT_DEFINITION ( 'UNKNOWN', '', #12094, #22022 ) ;
#33203=FACE_OUTER_BOUND ( 'NONE', #47, .T. ) ;
#33214=ORIENTED_EDGE ( 'NONE', *, *, #8681, .F. ) ;
#33292=DIRECTION ( 'NONE',  ( -0.000000000000000000, -0.000000000000000000, 1.000000000000000000 ) ) ;
#33303=ORIENTED_EDGE ( 'NONE', *, *, #33053, .F. ) ;
#33347=VECTOR ( 'NONE', #3828, 1000.000000000000000 ) ;
#33422=CIRCLE ( 'NONE', #18176, 1.650000000000000133 ) ;
#33467=ORIENTED_EDGE ( 'NONE', *, *, #13261, .T. ) ;
#33471=EDGE_LOOP ( 'NONE', ( #23660, #8535, #26756, #15890 ) ) ;
#33523=DIRECTION ( 'NONE',  ( -0.000000000000000000, -0.000000000000000000, 1.000000000000000000 ) ) ;
#33526=EDGE_CURVE ( 'NONE', #2969, #5005, #1301, .T. ) ;
#33539=DIRECTION ( 'NONE',  ( 1.000000000000000000, 0.000000000000000000, 0.000000000000000000 ) ) ;
#33624=VECTOR ( 'NONE', #24201, 1000.000000000000000 ) ;
#33640=ORIENTED_EDGE ( 'NONE', *, *, #24556, .T. ) ;
#33645=VERTEX_POINT ( 'NONE', #24082 ) ;
#33652=ADVANCED_FACE ( 'NONE', ( #29200 ), #418, .T. ) ;
ENDSEC;
END-ISO-10303-21;
